ISO-10303-21;
HEADER;
FILE_DESCRIPTION (('STEP AP214'),
    '1' );
FILE_NAME ('Central Rotary Housing.step',
    '2026-10-07T17:53:07',
    ( '' ),
    ( '' ),
    'SwSTEP 2.0',
    'SolidWorks 2025',
    '' );
FILE_SCHEMA (( 'AUTOMOTIVE_DESIGN' ));
ENDSEC;

DATA;
#5=LINE ( 'NONE', #10836, #6273 ) ;
#9=VECTOR ( 'NONE', #8104, 1000.000000000000000 ) ;
#11=AXIS2_PLACEMENT_3D ( 'NONE', #8934, #9983, #13191 ) ;
#15=ORIENTED_EDGE ( 'NONE', *, *, #6104, .F. ) ;
#18=VECTOR ( 'NONE', #2959, 1000.000000000000000 ) ;
#20=ORIENTED_EDGE ( 'NONE', *, *, #13229, .F. ) ;
#21=ORIENTED_EDGE ( 'NONE', *, *, #12073, .F. ) ;
#25=CARTESIAN_POINT ( 'NONE',  ( 43.38563590245419732, 87.34974178189119698, 20.00000000000000000 ) ) ;
#29=DIRECTION ( 'NONE',  ( 0.000000000000000000, -1.000000000000000000, 0.000000000000000000 ) ) ;
#38=CARTESIAN_POINT ( 'NONE',  ( 74.18094369249178044, 97.20665973629650125, 10.00000000000000000 ) ) ;
#45=CARTESIAN_POINT ( 'NONE',  ( 68.49370948373500312, 113.0390816101113387, 0.7500000000000006661 ) ) ;
#47=DIRECTION ( 'NONE',  ( -0.000000000000000000, -0.000000000000000000, -1.000000000000000000 ) ) ;
#54=VERTEX_POINT ( 'NONE', #10526 ) ;
#61=EDGE_CURVE ( 'NONE', #8730, #12568, #7625, .T. ) ;
#71=DIRECTION ( 'NONE',  ( -1.000000000000000000, 0.000000000000000000, -0.000000000000000000 ) ) ;
#72=CARTESIAN_POINT ( 'NONE',  ( 50.63563590245420443, 104.1554980190242361, 22.75000000000000000 ) ) ;
#73=LINE ( 'NONE', #12845, #11581 ) ;
#74=DIRECTION ( 'NONE',  ( 0.7071067811865451302, -0.7071067811865500152, 0.000000000000000000 ) ) ;
#75=EDGE_CURVE ( 'NONE', #10483, #2779, #7556, .T. ) ;
#81=FACE_OUTER_BOUND ( 'NONE', #12463, .T. ) ;
#85=DIRECTION ( 'NONE',  ( 0.000000000000000000, 0.000000000000000000, 1.000000000000000000 ) ) ;
#86=DIRECTION ( 'NONE',  ( 0.7071067811865525687, 0.7071067811865425767, -0.000000000000000000 ) ) ;
#88=EDGE_CURVE ( 'NONE', #10198, #10544, #1083, .T. ) ;
#89=CARTESIAN_POINT ( 'NONE',  ( 142.6356359024541973, 87.03908161011133870, 19.25000000000000000 ) ) ;
#100=DIRECTION ( 'NONE',  ( 0.000000000000000000, 0.000000000000000000, -1.000000000000000000 ) ) ;
#102=CARTESIAN_POINT ( 'NONE',  ( 44.76431555889455183, 85.34974178189114014, 2.983588460272618114E-16 ) ) ;
#106=CARTESIAN_POINT ( 'NONE',  ( 141.8856359024541973, 87.34974178189115435, 20.00000000000000000 ) ) ;
#108=CARTESIAN_POINT ( 'NONE',  ( 123.1053058165644671, 129.5087515242213669, 0.7500000000000000000 ) ) ;
#112=EDGE_CURVE ( 'NONE', #4329, #209, #6197, .T. ) ;
#119=DIRECTION ( 'NONE',  ( 0.000000000000000000, 0.000000000000000000, 1.000000000000000000 ) ) ;
#128=ADVANCED_FACE ( 'NONE', ( #1149 ), #7351, .F. ) ;
#135=VERTEX_POINT ( 'NONE', #8486 ) ;
#140=VECTOR ( 'NONE', #5917, 1000.000000000000114 ) ;
#141=DIRECTION ( 'NONE',  ( -0.000000000000000000, -0.000000000000000000, -1.000000000000000000 ) ) ;
#147=VECTOR ( 'NONE', #7020, 1000.000000000000000 ) ;
#155=EDGE_CURVE ( 'NONE', #8675, #3193, #8240, .T. ) ;
#174=DIRECTION ( 'NONE',  ( 1.000000000000000000, 0.000000000000000000, 0.000000000000000000 ) ) ;
#182=VERTEX_POINT ( 'NONE', #3404 ) ;
#183=ORIENTED_EDGE ( 'NONE', *, *, #11008, .T. ) ;
#187=EDGE_LOOP ( 'NONE', ( #9761, #8160, #4704, #9504 ) ) ;
#188=DIRECTION ( 'NONE',  ( -0.000000000000000000, -0.000000000000000000, 1.000000000000000000 ) ) ;
#190=FACE_OUTER_BOUND ( 'NONE', #11280, .T. ) ;
#198=VECTOR ( 'NONE', #6806, 999.9999999999998863 ) ;
#200=CARTESIAN_POINT ( 'NONE',  ( 62.16596598834396303, 68.56941169600129626, 20.00000000000000000 ) ) ;
#205=ADVANCED_FACE ( 'NONE', ( #704 ), #2436, .F. ) ;
#207=ORIENTED_EDGE ( 'NONE', *, *, #1883, .F. ) ;
#208=DIRECTION ( 'NONE',  ( 0.000000000000000000, 0.000000000000000000, 1.000000000000000000 ) ) ;
#209=VERTEX_POINT ( 'NONE', #11330 ) ;
#211=CARTESIAN_POINT ( 'NONE',  ( 42.63563590245419732, 87.03908161011136713, 0.7500000000000006661 ) ) ;
#212=FACE_OUTER_BOUND ( 'NONE', #7387, .T. ) ;
#217=VERTEX_POINT ( 'NONE', #6667 ) ;
#231=CYLINDRICAL_SURFACE ( 'NONE', #5745, 0.2500000000000002220 ) ;
#240=DIRECTION ( 'NONE',  ( 1.000000000000000000, 0.000000000000000000, 0.000000000000000000 ) ) ;
#242=AXIS2_PLACEMENT_3D ( 'NONE', #3348, #13046, #1170 ) ;
#243=VECTOR ( 'NONE', #2841, 1000.000000000000000 ) ;
#245=ORIENTED_EDGE ( 'NONE', *, *, #4667, .T. ) ;
#247=ADVANCED_FACE ( 'NONE', ( #9168 ), #6923, .T. ) ;
#251=EDGE_LOOP ( 'NONE', ( #7690, #10577, #8112, #1921 ) ) ;
#259=DIRECTION ( 'NONE',  ( 0.000000000000000000, 0.000000000000000000, 1.000000000000000000 ) ) ;
#262=CARTESIAN_POINT ( 'NONE',  ( 140.6356359024541973, 113.0390816101113245, 0.7500000000000000000 ) ) ;
#267=ORIENTED_EDGE ( 'NONE', *, *, #6326, .T. ) ;
#268=CIRCLE ( 'NONE', #8070, 9.999999999999994671 ) ;
#269=ORIENTED_EDGE ( 'NONE', *, *, #4933, .T. ) ;
#283=CARTESIAN_POINT ( 'NONE',  ( 101.4499059006094512, 83.97306027416853169, 10.00000000000000000 ) ) ;
#287=ORIENTED_EDGE ( 'NONE', *, *, #11211, .T. ) ;
#292=LINE ( 'NONE', #13064, #9783 ) ;
#299=EDGE_CURVE ( 'NONE', #2876, #6180, #11927, .T. ) ;
#304=EDGE_LOOP ( 'NONE', ( #3114, #10069, #6854, #8399 ) ) ;
#305=CIRCLE ( 'NONE', #3211, 2.000000000000001776 ) ;
#307=ORIENTED_EDGE ( 'NONE', *, *, #8975, .F. ) ;
#309=DIRECTION ( 'NONE',  ( -1.000000000000000000, -0.000000000000000000, -0.000000000000000000 ) ) ;
#310=ORIENTED_EDGE ( 'NONE', *, *, #10181, .F. ) ;
#323=LINE ( 'NONE', #455, #3746 ) ;
#332=EDGE_CURVE ( 'NONE', #6971, #4388, #4137, .T. ) ;
#343=CARTESIAN_POINT ( 'NONE',  ( 142.3249757306743675, 110.9104019536709274, 2.976040314969929885E-15 ) ) ;
#347=( BOUNDED_CURVE ( )  B_SPLINE_CURVE ( 3, ( #7217, #11495, #8211, #7157 ),
 .UNSPECIFIED., .F., .F. ) 
 B_SPLINE_CURVE_WITH_KNOTS ( ( 4, 4 ),
 ( 3.141592653589792672, 4.712388980384689674 ),
 .UNSPECIFIED. ) 
 CURVE ( )  GEOMETRIC_REPRESENTATION_ITEM ( )  RATIONAL_B_SPLINE_CURVE ( ( 1.000000000000000000, 0.8047378541243649375, 0.8047378541243649375, 1.000000000000000000 ) ) 
 REPRESENTATION_ITEM ( '' )  );
#352=DIRECTION ( 'NONE',  ( -0.000000000000000000, -0.000000000000000000, -1.000000000000000000 ) ) ;
#355=VECTOR ( 'NONE', #352, 1000.000000000000000 ) ;
#357=CARTESIAN_POINT ( 'NONE',  ( 50.63563590245420443, 89.90549801902423610, 23.00000000000000000 ) ) ;
#362=ORIENTED_EDGE ( 'NONE', *, *, #6475, .T. ) ;
#363=VERTEX_POINT ( 'NONE', #5176 ) ;
#365=ORIENTED_EDGE ( 'NONE', *, *, #11013, .F. ) ;
#371=ORIENTED_EDGE ( 'NONE', *, *, #6030, .T. ) ;
#375=FACE_OUTER_BOUND ( 'NONE', #11590, .T. ) ;
#384=DIRECTION ( 'NONE',  ( 0.000000000000000000, 0.000000000000000000, 1.000000000000000000 ) ) ;
#387=LINE ( 'NONE', #8914, #11403 ) ;
#389=CARTESIAN_POINT ( 'NONE',  ( 116.7775623211734342, 123.0390816101113245, 20.00000000000000000 ) ) ;
#392=ORIENTED_EDGE ( 'NONE', *, *, #10970, .T. ) ;
#395=EDGE_LOOP ( 'NONE', ( #2584, #2957, #7382, #3323 ) ) ;
#404=DIRECTION ( 'NONE',  ( 1.000000000000000000, -0.000000000000000000, 0.000000000000000000 ) ) ;
#405=LINE ( 'NONE', #3904, #7107 ) ;
#412=CIRCLE ( 'NONE', #8208, 24.04163056034261459 ) ;
#437=ORIENTED_EDGE ( 'NONE', *, *, #13232, .F. ) ;
#438=CARTESIAN_POINT ( 'NONE',  ( 44.63563590245420443, 108.9054980190242503, 23.00000000000000000 ) ) ;
#447=EDGE_CURVE ( 'NONE', #9970, #6077, #6564, .T. ) ;
#448=CARTESIAN_POINT ( 'NONE',  ( 102.2760581142613603, 115.9375248198690826, 20.00000000000000000 ) ) ;
#449=ORIENTED_EDGE ( 'NONE', *, *, #12076, .T. ) ;
#453=CARTESIAN_POINT ( 'NONE',  ( 44.88563590245420443, 108.6554980190242503, 23.00000000000000000 ) ) ;
#455=CARTESIAN_POINT ( 'NONE',  ( 134.6356359024541973, 103.9054980190242361, 20.00000000000000000 ) ) ;
#465=ADVANCED_FACE ( 'NONE', ( #5437 ), #9788, .T. ) ;
#468=EDGE_CURVE ( 'NONE', #5173, #11089, #3806, .T. ) ;
#478=CARTESIAN_POINT ( 'NONE',  ( 44.94629607423406270, 112.2890816101113387, 20.00000000000000000 ) ) ;
#505=CIRCLE ( 'NONE', #3415, 0.7500000000000000000 ) ;
#514=CARTESIAN_POINT ( 'NONE',  ( 116.7775623211734342, 85.78908161011133870, 0.000000000000000000 ) ) ;
#522=ORIENTED_EDGE ( 'NONE', *, *, #7912, .T. ) ;
#535=DIRECTION ( 'NONE',  ( 1.000000000000000000, 0.000000000000000000, 0.000000000000000000 ) ) ;
#536=ORIENTED_EDGE ( 'NONE', *, *, #8265, .F. ) ;
#540=DIRECTION ( 'NONE',  ( 1.000000000000000000, 0.000000000000000000, 0.000000000000000000 ) ) ;
#543=CARTESIAN_POINT ( 'NONE',  ( 134.6356359024541973, 108.9054980190242503, 22.75000000000000000 ) ) ;
#561=DIRECTION ( 'NONE',  ( -0.7050191076322684935, -0.7091883091770476710, 0.000000000000000000 ) ) ;
#570=CARTESIAN_POINT ( 'NONE',  ( 83.82136590429891498, 114.1051029460540605, 10.00000000000000000 ) ) ;
#572=DIRECTION ( 'NONE',  ( -1.000000000000000000, 0.000000000000000000, 0.000000000000000000 ) ) ;
#577=EDGE_CURVE ( 'NONE', #1997, #8730, #12223, .T. ) ;
#583=CARTESIAN_POINT ( 'NONE',  ( 134.6356359024541973, 94.90549801902425031, 22.75000000000000000 ) ) ;
#599=EDGE_CURVE ( 'NONE', #821, #11310, #9518, .T. ) ;
#600=CYLINDRICAL_SURFACE ( 'NONE', #3494, 10.00000000000000178 ) ;
#604=DIRECTION ( 'NONE',  ( 0.000000000000000000, 0.000000000000000000, 1.000000000000000000 ) ) ;
#610=CARTESIAN_POINT ( 'NONE',  ( 50.63563590245420443, 94.90549801902425031, 22.75000000000000000 ) ) ;
#612=CARTESIAN_POINT ( 'NONE',  ( 140.6356359024541973, 108.9054980190242503, 20.00000000000000000 ) ) ;
#618=EDGE_LOOP ( 'NONE', ( #4297, #9281, #12104, #1831, #7193, #7570, #5316, #11054, #1342, #8855, #9171, #9443, #11118, #5927, #3897, #4500 ) ) ;
#620=CARTESIAN_POINT ( 'NONE',  ( 134.7391892930474739, 104.0090514096174843, 23.00000000000000000 ) ) ;
#623=VECTOR ( 'NONE', #10124, 1000.000000000000000 ) ;
#629=ADVANCED_FACE ( 'NONE', ( #13264 ), #1537, .T. ) ;
#634=ORIENTED_EDGE ( 'NONE', *, *, #2585, .F. ) ;
#636=EDGE_CURVE ( 'NONE', #6971, #6593, #6837, .T. ) ;
#650=ADVANCED_FACE ( 'NONE', ( #11110 ), #5788, .F. ) ;
#655=FACE_OUTER_BOUND ( 'NONE', #13439, .T. ) ;
#656=LINE ( 'NONE', #12543, #7857 ) ;
#664=DIRECTION ( 'NONE',  ( -0.000000000000000000, -0.000000000000000000, -1.000000000000000000 ) ) ;
#667=CARTESIAN_POINT ( 'NONE',  ( 116.7775623211734342, 75.03908161011133870, 19.25000000000000000 ) ) ;
#674=VECTOR ( 'NONE', #141, 1000.000000000000000 ) ;
#675=CARTESIAN_POINT ( 'NONE',  ( 42.63563590245419732, 111.0390816101113387, 19.25000000000000000 ) ) ;
#678=DIRECTION ( 'NONE',  ( 0.000000000000000000, 0.000000000000000000, 1.000000000000000000 ) ) ;
#680=DIRECTION ( 'NONE',  ( 1.000000000000000000, 0.000000000000000000, 0.000000000000000000 ) ) ;
#682=AXIS2_PLACEMENT_3D ( 'NONE', #4209, #2406, #6504 ) ;
#691=LINE ( 'NONE', #9361, #8209 ) ;
#704=FACE_OUTER_BOUND ( 'NONE', #6355, .T. ) ;
#706=ORIENTED_EDGE ( 'NONE', *, *, #11105, .T. ) ;
#710=CYLINDRICAL_SURFACE ( 'NONE', #2943, 0.2500000000000002220 ) ;
#712=EDGE_CURVE ( 'NONE', #11588, #3512, #7345, .T. ) ;
#713=CARTESIAN_POINT ( 'NONE',  ( 44.63563590245420443, 103.9054980190242361, 20.00000000000000000 ) ) ;
#715=DIRECTION ( 'NONE',  ( 0.7071067811865382469, -0.7071067811865567876, 0.000000000000000000 ) ) ;
#719=VERTEX_POINT ( 'NONE', #10474 ) ;
#721=VERTEX_POINT ( 'NONE', #11382 ) ;
#728=DIRECTION ( 'NONE',  ( 0.000000000000000000, 1.000000000000000000, 0.000000000000000000 ) ) ;
#730=EDGE_CURVE ( 'NONE', #12176, #10198, #9359, .T. ) ;
#731=FACE_BOUND ( 'NONE', #2240, .T. ) ;
#757=CARTESIAN_POINT ( 'NONE',  ( 68.49370948373500312, 123.0390816101113245, 19.25000000000000000 ) ) ;
#761=ORIENTED_EDGE ( 'NONE', *, *, #2809, .F. ) ;
#764=ORIENTED_EDGE ( 'NONE', *, *, #8126, .F. ) ;
#770=EDGE_CURVE ( 'NONE', #2779, #11622, #3159, .T. ) ;
#772=ORIENTED_EDGE ( 'NONE', *, *, #10939, .F. ) ;
#786=VECTOR ( 'NONE', #7174, 1000.000000000000000 ) ;
#791=DIRECTION ( 'NONE',  ( 0.000000000000000000, 0.000000000000000000, 1.000000000000000000 ) ) ;
#792=AXIS2_PLACEMENT_3D ( 'NONE', #38, #8552, #2020 ) ;
#802=CARTESIAN_POINT ( 'NONE',  ( 112.1804561881462945, 85.03908161011133870, 20.00000000000000000 ) ) ;
#816=EDGE_CURVE ( 'NONE', #1026, #1798, #3028, .T. ) ;
#818=CARTESIAN_POINT ( 'NONE',  ( 50.38563590245420443, 104.1554980190242361, 23.00000000000000000 ) ) ;
#821=VERTEX_POINT ( 'NONE', #7238 ) ;
#827=DIRECTION ( 'NONE',  ( 0.000000000000000000, 0.000000000000000000, 1.000000000000000000 ) ) ;
#829=CARTESIAN_POINT ( 'NONE',  ( 44.76431555889458025, 85.34974178189114014, 20.00000000000000000 ) ) ;
#830=CARTESIAN_POINT ( 'NONE',  ( 105.4499059006094654, 83.97306027416853169, 20.00000000000000000 ) ) ;
#836=ORIENTED_EDGE ( 'NONE', *, *, #6900, .F. ) ;
#837=AXIS2_PLACEMENT_3D ( 'NONE', #9903, #13096, #3544 ) ;
#839=EDGE_LOOP ( 'NONE', ( #1003, #10345, #8315, #8505 ) ) ;
#840=LINE ( 'NONE', #4002, #9289 ) ;
#841=AXIS2_PLACEMENT_3D ( 'NONE', #2225, #1215, #100 ) ;
#844=ORIENTED_EDGE ( 'NONE', *, *, #10998, .T. ) ;
#856=ORIENTED_EDGE ( 'NONE', *, *, #4667, .F. ) ;
#862=ORIENTED_EDGE ( 'NONE', *, *, #3092, .T. ) ;
#871=( BOUNDED_CURVE ( )  B_SPLINE_CURVE ( 3, ( #25, #9523, #5193, #3122 ),
 .UNSPECIFIED., .F., .F. ) 
 B_SPLINE_CURVE_WITH_KNOTS ( ( 4, 4 ),
 ( 1.570796326794896558, 3.141592653589793116 ),
 .UNSPECIFIED. ) 
 CURVE ( )  GEOMETRIC_REPRESENTATION_ITEM ( )  RATIONAL_B_SPLINE_CURVE ( ( 1.000000000000000000, 0.8047378541243649375, 0.8047378541243649375, 1.000000000000000000 ) ) 
 REPRESENTATION_ITEM ( '' )  );
#878=VERTEX_POINT ( 'NONE', #1235 ) ;
#880=DIRECTION ( 'NONE',  ( 0.000000000000000000, 0.000000000000000000, 1.000000000000000000 ) ) ;
#881=LINE ( 'NONE', #10259, #7955 ) ;
#882=PLANE ( 'NONE',  #7158 ) ;
#883=CARTESIAN_POINT ( 'NONE',  ( 42.63563590245419732, 111.0390816101113103, 19.68933982822018081 ) ) ;
#885=CARTESIAN_POINT ( 'NONE',  ( 103.4499059006094512, 83.97306027416853169, 10.00000000000000000 ) ) ;
#895=EDGE_LOOP ( 'NONE', ( #3869, #7424, #13659, #2544 ) ) ;
#911=ORIENTED_EDGE ( 'NONE', *, *, #332, .F. ) ;
#917=PLANE ( 'NONE',  #4481 ) ;
#922=ORIENTED_EDGE ( 'NONE', *, *, #6084, .T. ) ;
#923=LINE ( 'NONE', #12005, #1345 ) ;
#931=AXIS2_PLACEMENT_3D ( 'NONE', #5128, #13652, #4994 ) ;
#932=ORIENTED_EDGE ( 'NONE', *, *, #13740, .F. ) ;
#933=ORIENTED_EDGE ( 'NONE', *, *, #4165, .F. ) ;
#935=ORIENTED_EDGE ( 'NONE', *, *, #9064, .F. ) ;
#939=VERTEX_POINT ( 'NONE', #8720 ) ;
#940=DIRECTION ( 'NONE',  ( 0.000000000000000000, 0.000000000000000000, 1.000000000000000000 ) ) ;
#941=PLANE ( 'NONE',  #5749 ) ;
#945=FACE_OUTER_BOUND ( 'NONE', #6346, .T. ) ;
#948=CARTESIAN_POINT ( 'NONE',  ( 68.49370948373500312, 113.0390816101113387, 19.25000000000000000 ) ) ;
#950=ADVANCED_FACE ( 'NONE', ( #5636 ), #10890, .F. ) ;
#958=CARTESIAN_POINT ( 'NONE',  ( 44.94629607423404849, 85.78908161011133870, 20.00000000000000000 ) ) ;
#960=( BOUNDED_CURVE ( )  B_SPLINE_CURVE ( 3, ( #7023, #6960, #883, #675 ),
 .UNSPECIFIED., .F., .F. ) 
 B_SPLINE_CURVE_WITH_KNOTS ( ( 4, 4 ),
 ( 4.712388980384689674, 6.283185307179586232 ),
 .UNSPECIFIED. ) 
 CURVE ( )  GEOMETRIC_REPRESENTATION_ITEM ( )  RATIONAL_B_SPLINE_CURVE ( ( 1.000000000000000000, 0.8047378541243649375, 0.8047378541243649375, 1.000000000000000000 ) ) 
 REPRESENTATION_ITEM ( '' )  );
#972=EDGE_CURVE ( 'NONE', #1552, #4825, #7152, .T. ) ;
#980=CARTESIAN_POINT ( 'NONE',  ( 134.7391892930474739, 94.80194462843097369, 23.00000000000000000 ) ) ;
#987=ORIENTED_EDGE ( 'NONE', *, *, #12687, .F. ) ;
#989=CARTESIAN_POINT ( 'NONE',  ( 43.38563590245419732, 87.34974178189119698, 0.000000000000000000 ) ) ;
#996=EDGE_LOOP ( 'NONE', ( #10152, #2242, #2087, #5658 ) ) ;
#1003=ORIENTED_EDGE ( 'NONE', *, *, #3652, .F. ) ;
#1014=VECTOR ( 'NONE', #9490, 1000.000000000000000 ) ;
#1015=DIRECTION ( 'NONE',  ( 1.000000000000000000, 0.000000000000000000, 0.000000000000000000 ) ) ;
#1019=FACE_OUTER_BOUND ( 'NONE', #11910, .T. ) ;
#1024=CARTESIAN_POINT ( 'NONE',  ( 68.49370948373500312, 75.03908161011133870, 20.00000000000000000 ) ) ;
#1026=VERTEX_POINT ( 'NONE', #1656 ) ;
#1033=DIRECTION ( 'NONE',  ( 0.7071067811865525687, 0.7071067811865425767, -0.000000000000000000 ) ) ;
#1039=CIRCLE ( 'NONE', #1255, 0.7500000000000000000 ) ;
#1044=CARTESIAN_POINT ( 'NONE',  ( 44.63563590245420443, 94.90549801902425031, 23.00000000000000000 ) ) ;
#1049=DIRECTION ( 'NONE',  ( 0.000000000000000000, 0.000000000000000000, 1.000000000000000000 ) ) ;
#1052=EDGE_CURVE ( 'NONE', #3941, #217, #10504, .T. ) ;
#1053=CIRCLE ( 'NONE', #4855, 2.000000000000001776 ) ;
#1054=ORIENTED_EDGE ( 'NONE', *, *, #13308, .T. ) ;
#1059=ORIENTED_EDGE ( 'NONE', *, *, #7926, .T. ) ;
#1062=CARTESIAN_POINT ( 'NONE',  ( 140.6356359024541973, 103.9054980190242361, 22.75000000000000000 ) ) ;
#1063=ORIENTED_EDGE ( 'NONE', *, *, #4240, .F. ) ;
#1073=ORIENTED_EDGE ( 'NONE', *, *, #10346, .F. ) ;
#1083=LINE ( 'NONE', #2086, #7729 ) ;
#1084=CARTESIAN_POINT ( 'NONE',  ( 113.0903281124166710, 100.8715034839261762, 20.00000000000000000 ) ) ;
#1092=AXIS2_PLACEMENT_3D ( 'NONE', #8296, #4044, #1942 ) ;
#1096=ORIENTED_EDGE ( 'NONE', *, *, #5921, .F. ) ;
#1097=CARTESIAN_POINT ( 'NONE',  ( 116.7775623211734342, 123.0390816101113245, 0.000000000000000000 ) ) ;
#1100=CARTESIAN_POINT ( 'NONE',  ( 134.6356359024541973, 94.90549801902425031, 20.00000000000000000 ) ) ;
#1103=TOROIDAL_SURFACE ( 'NONE', #5141, 23.29163056034262169, 0.7500000000000000000 ) ;
#1109=VERTEX_POINT ( 'NONE', #1449 ) ;
#1117=AXIS2_PLACEMENT_3D ( 'NONE', #12921, #6570, #10841 ) ;
#1127=VECTOR ( 'NONE', #13305, 1000.000000000000000 ) ;
#1129=ORIENTED_EDGE ( 'NONE', *, *, #9612, .T. ) ;
#1131=ADVANCED_FACE ( 'NONE', ( #5769 ), #10054, .T. ) ;
#1132=DIRECTION ( 'NONE',  ( 0.000000000000000000, 0.000000000000000000, -1.000000000000000000 ) ) ;
#1138=CARTESIAN_POINT ( 'NONE',  ( 44.63563590245422574, 112.2890816101113387, 20.00000000000000000 ) ) ;
#1145=VECTOR ( 'NONE', #13775, 1000.000000000000000 ) ;
#1149=FACE_OUTER_BOUND ( 'NONE', #5234, .T. ) ;
#1150=DIRECTION ( 'NONE',  ( 0.000000000000000000, 1.000000000000000000, -0.000000000000000000 ) ) ;
#1165=ORIENTED_EDGE ( 'NONE', *, *, #3279, .F. ) ;
#1169=CIRCLE ( 'NONE', #4309, 10.74999999999999645 ) ;
#1170=DIRECTION ( 'NONE',  ( 1.000000000000000000, 0.000000000000000000, 0.000000000000000000 ) ) ;
#1173=CARTESIAN_POINT ( 'NONE',  ( 83.82136590429891498, 114.1051029460540605, 10.00000000000000000 ) ) ;
#1176=ADVANCED_FACE ( 'NONE', ( #4173 ), #882, .F. ) ;
#1187=CARTESIAN_POINT ( 'NONE',  ( 74.18094369249178044, 97.20665973629650125, 20.00000000000000000 ) ) ;
#1188=LINE ( 'NONE', #6508, #1300 ) ;
#1194=EDGE_LOOP ( 'NONE', ( #2877, #4120 ) ) ;
#1200=DIRECTION ( 'NONE',  ( -1.000000000000000000, 0.000000000000000000, 0.000000000000000000 ) ) ;
#1208=ORIENTED_EDGE ( 'NONE', *, *, #7558, .F. ) ;
#1212=VERTEX_POINT ( 'NONE', #7285 ) ;
#1215=DIRECTION ( 'NONE',  ( 1.000000000000000000, 0.000000000000000000, 0.000000000000000000 ) ) ;
#1221=DIRECTION ( 'NONE',  ( 0.000000000000000000, 0.000000000000000000, 1.000000000000000000 ) ) ;
#1223=CARTESIAN_POINT ( 'NONE',  ( 113.0903281124166710, 100.8715034839261762, 10.00000000000000000 ) ) ;
#1225=EDGE_CURVE ( 'NONE', #4495, #721, #6178, .T. ) ;
#1229=CARTESIAN_POINT ( 'NONE',  ( 50.63563590245420443, 103.9054980190242361, 22.75000000000000000 ) ) ;
#1233=ORIENTED_EDGE ( 'NONE', *, *, #10224, .T. ) ;
#1235=CARTESIAN_POINT ( 'NONE',  ( 76.11748380738829667, 82.61803701715820125, 0.000000000000000000 ) ) ;
#1237=DIRECTION ( 'NONE',  ( -0.000000000000000000, 1.000000000000000000, -0.000000000000000000 ) ) ;
#1239=AXIS2_PLACEMENT_3D ( 'NONE', #13784, #5466, #12756 ) ;
#1254=DIRECTION ( 'NONE',  ( 0.000000000000000000, 0.000000000000000000, -1.000000000000000000 ) ) ;
#1255=AXIS2_PLACEMENT_3D ( 'NONE', #10138, #9994, #12087 ) ;
#1256=CARTESIAN_POINT ( 'NONE',  ( 44.63563590245420443, 108.9054980190242503, 23.00000000000000000 ) ) ;
#1257=EDGE_CURVE ( 'NONE', #1798, #10620, #10323, .T. ) ;
#1263=VERTEX_POINT ( 'NONE', #7089 ) ;
#1271=CARTESIAN_POINT ( 'NONE',  ( 68.49370948373500312, 75.03908161011133870, 20.00000000000000000 ) ) ;
#1278=COLOUR_RGB ( '', 0.08235294, 0.09019608, 0.10196078) ;
#1285=DIRECTION ( 'NONE',  ( 1.000000000000000000, 0.000000000000000000, 0.000000000000000000 ) ) ;
#1289=SURFACE_STYLE_USAGE ( .BOTH. , #6335 ) ;
#1297=AXIS2_PLACEMENT_3D ( 'NONE', #13466, #11306, #1730 ) ;
#1299=VECTOR ( 'NONE', #10129, 1000.000000000000000 ) ;
#1300=VECTOR ( 'NONE', #8327, 1000.000000000000000 ) ;
#1301=VERTEX_POINT ( 'NONE', #2227 ) ;
#1305=DIRECTION ( 'NONE',  ( 1.000000000000000000, 0.000000000000000000, 0.000000000000000000 ) ) ;
#1310=EDGE_CURVE ( 'NONE', #135, #7821, #13435, .T. ) ;
#1312=AXIS2_PLACEMENT_3D ( 'NONE', #2805, #7025, #13669 ) ;
#1314=ADVANCED_FACE ( 'NONE', ( #1019 ), #4448, .F. ) ;
#1318=PLANE ( 'NONE',  #4202 ) ;
#1320=VECTOR ( 'NONE', #4212, 1000.000000000000000 ) ;
#1322=VECTOR ( 'NONE', #5683, 1000.000000000000000 ) ;
#1328=DIRECTION ( 'NONE',  ( 0.000000000000000000, 0.000000000000000000, 1.000000000000000000 ) ) ;
#1331=ADVANCED_FACE ( 'NONE', ( #8274 ), #6161, .F. ) ;
#1340=ORIENTED_EDGE ( 'NONE', *, *, #10711, .F. ) ;
#1342=ORIENTED_EDGE ( 'NONE', *, *, #10202, .T. ) ;
#1343=VECTOR ( 'NONE', #1033, 999.9999999999998863 ) ;
#1345=VECTOR ( 'NONE', #10978, 1000.000000000000000 ) ;
#1350=FACE_OUTER_BOUND ( 'NONE', #10782, .T. ) ;
#1356=EDGE_LOOP ( 'NONE', ( #10786, #1413, #10050, #4133 ) ) ;
#1357=ORIENTED_EDGE ( 'NONE', *, *, #11759, .T. ) ;
#1365=ADVANCED_FACE ( 'NONE', ( #655 ), #13575, .T. ) ;
#1369=ORIENTED_EDGE ( 'NONE', *, *, #155, .T. ) ;
#1381=LINE ( 'NONE', #5632, #3349 ) ;
#1382=ORIENTED_EDGE ( 'NONE', *, *, #4879, .F. ) ;
#1401=FACE_OUTER_BOUND ( 'NONE', #4521, .T. ) ;
#1409=EDGE_LOOP ( 'NONE', ( #8506, #3866, #11058, #3386 ) ) ;
#1413=ORIENTED_EDGE ( 'NONE', *, *, #11360, .F. ) ;
#1416=ORIENTED_EDGE ( 'NONE', *, *, #599, .T. ) ;
#1419=DIRECTION ( 'NONE',  ( -0.000000000000000000, -0.000000000000000000, 1.000000000000000000 ) ) ;
#1432=EDGE_CURVE ( 'NONE', #5796, #2636, #4422, .T. ) ;
#1438=FACE_BOUND ( 'NONE', #6006, .T. ) ;
#1444=DIRECTION ( 'NONE',  ( -0.000000000000000000, -0.000000000000000000, 1.000000000000000000 ) ) ;
#1447=EDGE_CURVE ( 'NONE', #6660, #9517, #3124, .T. ) ;
#1449=CARTESIAN_POINT ( 'NONE',  ( 42.63563590245419732, 111.0390816101113387, 0.7500000000000006661 ) ) ;
#1450=CARTESIAN_POINT ( 'NONE',  ( 112.1804561881462945, 112.2890816101113387, 0.7500000000000006661 ) ) ;
#1456=VECTOR ( 'NONE', #11799, 1000.000000000000000 ) ;
#1458=ORIENTED_EDGE ( 'NONE', *, *, #1257, .T. ) ;
#1464=VECTOR ( 'NONE', #2656, 1000.000000000000000 ) ;
#1469=LINE ( 'NONE', #12164, #4699 ) ;
#1472=ORIENTED_EDGE ( 'NONE', *, *, #10632, .T. ) ;
#1474=EDGE_LOOP ( 'NONE', ( #536, #2988, #9030, #307 ) ) ;
#1475=ORIENTED_EDGE ( 'NONE', *, *, #8339, .T. ) ;
#1479=ORIENTED_EDGE ( 'NONE', *, *, #9694, .T. ) ;
#1481=ORIENTED_EDGE ( 'NONE', *, *, #577, .T. ) ;
#1492=DIRECTION ( 'NONE',  ( -0.000000000000000000, -0.000000000000000000, 1.000000000000000000 ) ) ;
#1498=DIRECTION ( 'NONE',  ( 0.000000000000000000, 0.000000000000000000, 1.000000000000000000 ) ) ;
#1503=ORIENTED_EDGE ( 'NONE', *, *, #3611, .F. ) ;
#1504=ADVANCED_FACE ( 'NONE', ( #11829 ), #4229, .F. ) ;
#1509=DIRECTION ( 'NONE',  ( 0.000000000000000000, 0.000000000000000000, 1.000000000000000000 ) ) ;
#1533=AXIS2_PLACEMENT_3D ( 'NONE', #12415, #2868, #7092 ) ;
#1537=CYLINDRICAL_SURFACE ( 'NONE', #10957, 0.7500000000000000000 ) ;
#1552=VERTEX_POINT ( 'NONE', #7683 ) ;
#1567=VERTEX_POINT ( 'NONE', #7763 ) ;
#1568=CARTESIAN_POINT ( 'NONE',  ( 101.4499059006094512, 83.97306027416853169, 10.00000000000000000 ) ) ;
#1569=VERTEX_POINT ( 'NONE', #6930 ) ;
#1573=CARTESIAN_POINT ( 'NONE',  ( 140.6356359024541973, 89.90549801902423610, 23.00000000000000000 ) ) ;
#1583=DIRECTION ( 'NONE',  ( 0.000000000000000000, 0.000000000000000000, 1.000000000000000000 ) ) ;
#1585=CARTESIAN_POINT ( 'NONE',  ( 116.7775623211734342, 85.03908161011133870, 0.7500000000000006661 ) ) ;
#1593=DIRECTION ( 'NONE',  ( 0.000000000000000000, -1.000000000000000000, 0.000000000000000000 ) ) ;
#1596=CARTESIAN_POINT ( 'NONE',  ( 50.63563590245420443, 108.9054980190242503, 22.75000000000000000 ) ) ;
#1599=AXIS2_PLACEMENT_3D ( 'NONE', #2786, #1786, #7208 ) ;
#1603=ORIENTED_EDGE ( 'NONE', *, *, #8859, .F. ) ;
#1606=ORIENTED_EDGE ( 'NONE', *, *, #13740, .T. ) ;
#1609=DIRECTION ( 'NONE',  ( 1.000000000000000000, 0.000000000000000000, 0.000000000000000000 ) ) ;
#1612=CARTESIAN_POINT ( 'NONE',  ( 68.49370948373500312, 123.0390816101113245, 0.000000000000000000 ) ) ;
#1614=DIRECTION ( 'NONE',  ( 0.000000000000000000, 1.000000000000000000, -0.000000000000000000 ) ) ;
#1616=ADVANCED_FACE ( 'NONE', ( #1628 ), #10158, .F. ) ;
#1617=EDGE_LOOP ( 'NONE', ( #1773, #7606, #6309, #2503 ) ) ;
#1625=DIRECTION ( 'NONE',  ( -0.000000000000000000, 0.000000000000000000, -1.000000000000000000 ) ) ;
#1627=ADVANCED_FACE ( 'NONE', ( #3602 ), #13288, .F. ) ;
#1628=FACE_OUTER_BOUND ( 'NONE', #9221, .T. ) ;
#1632=CARTESIAN_POINT ( 'NONE',  ( 140.3856359024541973, 104.1554980190242361, 23.00000000000000000 ) ) ;
#1650=LINE ( 'NONE', #5897, #9500 ) ;
#1651=CARTESIAN_POINT ( 'NONE',  ( 134.6356359024541973, 89.90549801902423610, 22.75000000000000000 ) ) ;
#1656=CARTESIAN_POINT ( 'NONE',  ( 116.7775623211734342, 113.0390816101113387, 0.7500000000000006661 ) ) ;
#1669=CYLINDRICAL_SURFACE ( 'NONE', #2379, 24.04163056034261459 ) ;
#1680=DIRECTION ( 'NONE',  ( 0.000000000000000000, 0.000000000000000000, -1.000000000000000000 ) ) ;
#1684=VECTOR ( 'NONE', #5986, 1000.000000000000000 ) ;
#1697=CARTESIAN_POINT ( 'NONE',  ( 140.6356359024541973, 103.9054980190242361, 22.89644660940672694 ) ) ;
#1698=EDGE_CURVE ( 'NONE', #6077, #12394, #12449, .T. ) ;
#1700=ADVANCED_FACE ( 'NONE', ( #11407 ), #710, .T. ) ;
#1702=ORIENTED_EDGE ( 'NONE', *, *, #11140, .T. ) ;
#1717=ORIENTED_EDGE ( 'NONE', *, *, #3656, .T. ) ;
#1723=DIRECTION ( 'NONE',  ( 1.000000000000000000, 0.000000000000000000, 0.000000000000000000 ) ) ;
#1726=CARTESIAN_POINT ( 'NONE',  ( 134.6356359024541973, 108.9054980190242503, 20.00000000000000000 ) ) ;
#1727=CARTESIAN_POINT ( 'NONE',  ( 116.7775623211734342, 123.0390816101113245, 19.25000000000000000 ) ) ;
#1730=DIRECTION ( 'NONE',  ( 1.000000000000000000, 0.000000000000000000, 0.000000000000000000 ) ) ;
#1732=ADVANCED_FACE ( 'NONE', ( #2908 ), #10420, .T. ) ;
#1736=CARTESIAN_POINT ( 'NONE',  ( 44.73918929304747394, 90.00905140961751272, 23.00000000000000000 ) ) ;
#1747=DIRECTION ( 'NONE',  ( 0.000000000000000000, 0.000000000000000000, 1.000000000000000000 ) ) ;
#1759=ORIENTED_EDGE ( 'NONE', *, *, #13685, .F. ) ;
#1766=ORIENTED_EDGE ( 'NONE', *, *, #3092, .F. ) ;
#1767=DIRECTION ( 'NONE',  ( 1.000000000000000000, 0.000000000000000000, 0.000000000000000000 ) ) ;
#1768=CARTESIAN_POINT ( 'NONE',  ( 134.6356359024541973, 103.9054980190242361, 23.00000000000000000 ) ) ;
#1771=CARTESIAN_POINT ( 'NONE',  ( 44.63563590245421864, 85.03908161011133870, 0.7500000000000000000 ) ) ;
#1773=ORIENTED_EDGE ( 'NONE', *, *, #61, .T. ) ;
#1777=EDGE_CURVE ( 'NONE', #11822, #7821, #6148, .T. ) ;
#1778=LINE ( 'NONE', #9313, #243 ) ;
#1779=( BOUNDED_CURVE ( )  B_SPLINE_CURVE ( 3, ( #12956, #11769, #8621, #9542 ),
 .UNSPECIFIED., .F., .F. ) 
 B_SPLINE_CURVE_WITH_KNOTS ( ( 4, 4 ),
 ( 3.141592653589793116, 4.712388980384689674 ),
 .UNSPECIFIED. ) 
 CURVE ( )  GEOMETRIC_REPRESENTATION_ITEM ( )  RATIONAL_B_SPLINE_CURVE ( ( 1.000000000000000000, 0.8047378541243649375, 0.8047378541243649375, 1.000000000000000000 ) ) 
 REPRESENTATION_ITEM ( '' )  );
#1786=DIRECTION ( 'NONE',  ( -0.000000000000000000, -0.000000000000000000, 1.000000000000000000 ) ) ;
#1788=LINE ( 'NONE', #5892, #3741 ) ;
#1794=AXIS2_PLACEMENT_3D ( 'NONE', #7342, #5199, #7546 ) ;
#1798=VERTEX_POINT ( 'NONE', #12593 ) ;
#1811=DIRECTION ( 'NONE',  ( 0.000000000000000000, 0.000000000000000000, 1.000000000000000000 ) ) ;
#1817=ORIENTED_EDGE ( 'NONE', *, *, #5404, .F. ) ;
#1819=EDGE_LOOP ( 'NONE', ( #6252, #4124, #2486, #10182 ) ) ;
#1827=FACE_OUTER_BOUND ( 'NONE', #10780, .T. ) ;
#1831=ORIENTED_EDGE ( 'NONE', *, *, #6135, .T. ) ;
#1833=CIRCLE ( 'NONE', #5609, 2.000000000000001776 ) ;
#1837=CARTESIAN_POINT ( 'NONE',  ( 92.63563590245421153, 85.78908161011133870, 19.25000000000000000 ) ) ;
#1840=DIRECTION ( 'NONE',  ( 0.000000000000000000, 0.000000000000000000, 1.000000000000000000 ) ) ;
#1841=ORIENTED_EDGE ( 'NONE', *, *, #12911, .F. ) ;
#1842=DIRECTION ( 'NONE',  ( 0.000000000000000000, 0.000000000000000000, 1.000000000000000000 ) ) ;
#1861=CARTESIAN_POINT ( 'NONE',  ( 44.63563590245420443, 94.90549801902425031, 22.75000000000000000 ) ) ;
#1869=ORIENTED_EDGE ( 'NONE', *, *, #3418, .T. ) ;
#1872=LINE ( 'NONE', #12556, #7490 ) ;
#1877=DIRECTION ( 'NONE',  ( -0.000000000000000000, -1.000000000000000000, 0.000000000000000000 ) ) ;
#1880=CARTESIAN_POINT ( 'NONE',  ( 134.6356359024541973, 103.9054980190242361, 22.75000000000000000 ) ) ;
#1883=EDGE_CURVE ( 'NONE', #1954, #4388, #923, .T. ) ;
#1885=ADVANCED_FACE ( 'NONE', ( #12077 ), #3808, .T. ) ;
#1886=ORIENTED_EDGE ( 'NONE', *, *, #12222, .F. ) ;
#1893=CARTESIAN_POINT ( 'NONE',  ( 74.18094369249178044, 97.20665973629650125, 10.00000000000000000 ) ) ;
#1894=CARTESIAN_POINT ( 'NONE',  ( 44.94629607423404849, 85.78908161011133870, 20.00000000000000000 ) ) ;
#1895=DIRECTION ( 'NONE',  ( -1.000000000000000000, -0.000000000000000000, 0.000000000000000000 ) ) ;
#1897=EDGE_CURVE ( 'NONE', #7689, #4189, #7657, .T. ) ;
#1901=ORIENTED_EDGE ( 'NONE', *, *, #4528, .F. ) ;
#1902=CARTESIAN_POINT ( 'NONE',  ( 142.6356359024541973, 87.03908161011133870, 0.7500000000000000000 ) ) ;
#1915=EDGE_CURVE ( 'NONE', #1552, #3512, #11940, .T. ) ;
#1916=ORIENTED_EDGE ( 'NONE', *, *, #1432, .T. ) ;
#1921=ORIENTED_EDGE ( 'NONE', *, *, #10224, .F. ) ;
#1926=FACE_BOUND ( 'NONE', #3735, .T. ) ;
#1928=ORIENTED_EDGE ( 'NONE', *, *, #12110, .F. ) ;
#1939=ORIENTED_EDGE ( 'NONE', *, *, #2072, .T. ) ;
#1942=DIRECTION ( 'NONE',  ( 1.000000000000000000, 0.000000000000000000, 0.000000000000000000 ) ) ;
#1943=DIRECTION ( 'NONE',  ( -0.000000000000000000, -0.000000000000000000, 1.000000000000000000 ) ) ;
#1945=VECTOR ( 'NONE', #5991, 1000.000000000000000 ) ;
#1953=AXIS2_PLACEMENT_3D ( 'NONE', #4110, #7283, #3007 ) ;
#1954=VERTEX_POINT ( 'NONE', #6555 ) ;
#1966=CARTESIAN_POINT ( 'NONE',  ( 44.63563590245422574, 85.03908161011132449, 19.68933982822018081 ) ) ;
#1967=VECTOR ( 'NONE', #10580, 1000.000000000000000 ) ;
#1973=VECTOR ( 'NONE', #3198, 1000.000000000000000 ) ;
#1974=ORIENTED_EDGE ( 'NONE', *, *, #4373, .F. ) ;
#1979=VECTOR ( 'NONE', #86, 999.9999999999998863 ) ;
#1988=ADVANCED_FACE ( 'NONE', ( #8014 ), #3840, .T. ) ;
#1993=VECTOR ( 'NONE', #11098, 1000.000000000000000 ) ;
#1997=VERTEX_POINT ( 'NONE', #610 ) ;
#1998=VERTEX_POINT ( 'NONE', #12289 ) ;
#2001=TOROIDAL_SURFACE ( 'NONE', #10915, 23.29163056034262169, 0.7500000000000000000 ) ;
#2004=CARTESIAN_POINT ( 'NONE',  ( 68.49370948373500312, 123.0390816101113245, 19.25000000000000000 ) ) ;
#2011=LINE ( 'NONE', #2926, #13639 ) ;
#2020=DIRECTION ( 'NONE',  ( 1.000000000000000000, 0.000000000000000000, 0.000000000000000000 ) ) ;
#2033=AXIS2_PLACEMENT_3D ( 'NONE', #8135, #12344, #5129 ) ;
#2035=ORIENTED_EDGE ( 'NONE', *, *, #11360, .T. ) ;
#2047=AXIS2_PLACEMENT_3D ( 'NONE', #10452, #880, #5138 ) ;
#2053=ORIENTED_EDGE ( 'NONE', *, *, #4933, .F. ) ;
#2057=AXIS2_PLACEMENT_3D ( 'NONE', #13251, #3691, #7934 ) ;
#2062=DIRECTION ( 'NONE',  ( 0.000000000000000000, -1.000000000000000000, 0.000000000000000000 ) ) ;
#2069=ORIENTED_EDGE ( 'NONE', *, *, #6084, .F. ) ;
#2072=EDGE_CURVE ( 'NONE', #12394, #2952, #10265, .T. ) ;
#2076=CARTESIAN_POINT ( 'NONE',  ( 44.73918929304747394, 94.80194462843097369, 23.00000000000000000 ) ) ;
#2078=DIRECTION ( 'NONE',  ( 0.000000000000000000, 1.000000000000000000, -0.000000000000000000 ) ) ;
#2079=CYLINDRICAL_SURFACE ( 'NONE', #11541, 0.2500000000000002220 ) ;
#2086=CARTESIAN_POINT ( 'NONE',  ( 92.63563590245421153, 112.2890816101113387, 0.000000000000000000 ) ) ;
#2087=ORIENTED_EDGE ( 'NONE', *, *, #8859, .T. ) ;
#2089=CARTESIAN_POINT ( 'NONE',  ( 62.16596598834446752, 129.5087515242215090, 0.7500000000000000000 ) ) ;
#2098=( LENGTH_UNIT ( ) NAMED_UNIT ( * ) SI_UNIT ( .MILLI., .METRE. ) );
#2099=ORIENTED_EDGE ( 'NONE', *, *, #8375, .F. ) ;
#2100=EDGE_LOOP ( 'NONE', ( #1916, #2103, #11395, #3232 ) ) ;
#2101=TOROIDAL_SURFACE ( 'NONE', #4765, 10.75000000000000000, 0.7500000000000000000 ) ;
#2102=FACE_OUTER_BOUND ( 'NONE', #11298, .T. ) ;
#2103=ORIENTED_EDGE ( 'NONE', *, *, #7329, .F. ) ;
#2107=CARTESIAN_POINT ( 'NONE',  ( 116.7775623211734342, 113.0390816101113387, 20.00000000000000000 ) ) ;
#2112=ADVANCED_FACE ( 'NONE', ( #9004 ), #12213, .T. ) ;
#2116=EDGE_LOOP ( 'NONE', ( #911, #6984, #11746, #6787 ) ) ;
#2119=DIRECTION ( 'NONE',  ( -0.000000000000000000, -1.000000000000000000, 0.000000000000000000 ) ) ;
#2122=DIRECTION ( 'NONE',  ( 1.000000000000000000, 0.000000000000000000, 0.000000000000000000 ) ) ;
#2124=EDGE_CURVE ( 'NONE', #4612, #4329, #10080, .T. ) ;
#2132=ORIENTED_EDGE ( 'NONE', *, *, #5350, .T. ) ;
#2133=ORIENTED_EDGE ( 'NONE', *, *, #6193, .T. ) ;
#2137=LINE ( 'NONE', #9464, #13121 ) ;
#2163=CIRCLE ( 'NONE', #11729, 6.000000000000005329 ) ;
#2164=EDGE_CURVE ( 'NONE', #2876, #11929, #5009, .T. ) ;
#2170=DIRECTION ( 'NONE',  ( 0.000000000000000000, 0.000000000000000000, 1.000000000000000000 ) ) ;
#2183=VERTEX_POINT ( 'NONE', #10595 ) ;
#2184=ORIENTED_EDGE ( 'NONE', *, *, #13109, .F. ) ;
#2188=DIRECTION ( 'NONE',  ( -0.7071067811865451302, 0.7071067811865500152, 0.000000000000000000 ) ) ;
#2192=CYLINDRICAL_SURFACE ( 'NONE', #12922, 0.2500000000000002220 ) ;
#2199=AXIS2_PLACEMENT_3D ( 'NONE', #6743, #7914, #12263 ) ;
#2200=ORIENTED_EDGE ( 'NONE', *, *, #3509, .F. ) ;
#2207=PRODUCT_DEFINITION ( 'UNKNOWN', '', #12909, #7100 ) ;
#2210=FACE_OUTER_BOUND ( 'NONE', #2874, .T. ) ;
#2215=CARTESIAN_POINT ( 'NONE',  ( 140.6356359024541973, 94.90549801902425031, 22.75000000000000000 ) ) ;
#2218=AXIS2_PLACEMENT_3D ( 'NONE', #2537, #2600, #11166 ) ;
#2220=VECTOR ( 'NONE', #4246, 1000.000000000000000 ) ;
#2221=VERTEX_POINT ( 'NONE', #9424 ) ;
#2224=FACE_OUTER_BOUND ( 'NONE', #6481, .T. ) ;
#2225=CARTESIAN_POINT ( 'NONE',  ( 0.000000000000000000, 94.65549801902425031, 22.75000000000000000 ) ) ;
#2227=CARTESIAN_POINT ( 'NONE',  ( 109.6856792294029219, 82.08927268643400055, 19.25000000000000000 ) ) ;
#2229=EDGE_LOOP ( 'NONE', ( #12559, #13234, #6292, #1717 ) ) ;
#2237=LINE ( 'NONE', #8567, #1014 ) ;
#2240=EDGE_LOOP ( 'NONE', ( #8583, #3718, #310, #1759 ) ) ;
#2241=EDGE_LOOP ( 'NONE', ( #12437, #1063, #6773, #2916 ) ) ;
#2242=ORIENTED_EDGE ( 'NONE', *, *, #11842, .T. ) ;
#2255=PRODUCT ( 'Central Rotary Housing', 'Central Rotary Housing', '', ( #4306 ) ) ;
#2267=CARTESIAN_POINT ( 'NONE',  ( 140.6356359024541973, 113.0390816101113387, 0.7500000000000006661 ) ) ;
#2273=DIRECTION ( 'NONE',  ( 0.000000000000000000, 0.000000000000000000, -1.000000000000000000 ) ) ;
#2275=FACE_OUTER_BOUND ( 'NONE', #13006, .T. ) ;
#2276=EDGE_LOOP ( 'NONE', ( #634, #6515 ) ) ;
#2284=CARTESIAN_POINT ( 'NONE',  ( 44.63563590245420443, 94.90549801902425031, 22.75000000000000000 ) ) ;
#2286=LINE ( 'NONE', #7466, #1973 ) ;
#2289=DIRECTION ( 'NONE',  ( -0.000000000000000000, -0.000000000000000000, -1.000000000000000000 ) ) ;
#2304=CYLINDRICAL_SURFACE ( 'NONE', #8227, 0.2500000000000002220 ) ;
#2309=EDGE_CURVE ( 'NONE', #4982, #11879, #8778, .T. ) ;
#2310=VECTOR ( 'NONE', #10660, 1000.000000000000000 ) ;
#2314=DIRECTION ( 'NONE',  ( 0.000000000000000000, 0.000000000000000000, 1.000000000000000000 ) ) ;
#2325=CARTESIAN_POINT ( 'NONE',  ( 116.7775623211734342, 85.03908161011133870, 0.000000000000000000 ) ) ;
#2329=( BOUNDED_CURVE ( )  B_SPLINE_CURVE ( 3, ( #11502, #3964, #13460, #11369 ),
 .UNSPECIFIED., .F., .F. ) 
 B_SPLINE_CURVE_WITH_KNOTS ( ( 4, 4 ),
 ( 3.141592653589793116, 4.712388980384689674 ),
 .UNSPECIFIED. ) 
 CURVE ( )  GEOMETRIC_REPRESENTATION_ITEM ( )  RATIONAL_B_SPLINE_CURVE ( ( 1.000000000000000000, 0.8047378541243649375, 0.8047378541243649375, 1.000000000000000000 ) ) 
 REPRESENTATION_ITEM ( '' )  );
#2356=DIRECTION ( 'NONE',  ( -1.000000000000000000, 0.000000000000000000, 0.000000000000000000 ) ) ;
#2362=ORIENTED_EDGE ( 'NONE', *, *, #816, .F. ) ;
#2363=EDGE_CURVE ( 'NONE', #9517, #9584, #3821, .T. ) ;
#2365=DIRECTION ( 'NONE',  ( 1.000000000000000000, 0.000000000000000000, 0.000000000000000000 ) ) ;
#2369=FACE_OUTER_BOUND ( 'NONE', #1819, .T. ) ;
#2375=DIRECTION ( 'NONE',  ( -0.000000000000000000, -0.000000000000000000, -1.000000000000000000 ) ) ;
#2377=DIRECTION ( 'NONE',  ( 1.000000000000000000, 0.000000000000000000, 0.000000000000000000 ) ) ;
#2379=AXIS2_PLACEMENT_3D ( 'NONE', #13326, #13199, #7946 ) ;
#2385=EDGE_CURVE ( 'NONE', #5130, #13231, #387, .T. ) ;
#2397=ORIENTED_EDGE ( 'NONE', *, *, #1225, .F. ) ;
#2402=EDGE_LOOP ( 'NONE', ( #7013, #8334, #3909, #6606 ) ) ;
#2404=EDGE_CURVE ( 'NONE', #13749, #4490, #13171, .T. ) ;
#2406=DIRECTION ( 'NONE',  ( -1.000000000000000000, 0.000000000000000000, -0.000000000000000000 ) ) ;
#2410=( BOUNDED_CURVE ( )  B_SPLINE_CURVE ( 3, ( #5641, #343, #8015, #5847 ),
 .UNSPECIFIED., .F., .F. ) 
 B_SPLINE_CURVE_WITH_KNOTS ( ( 4, 4 ),
 ( 4.712388980384695891, 6.283185307179586232 ),
 .UNSPECIFIED. ) 
 CURVE ( )  GEOMETRIC_REPRESENTATION_ITEM ( )  RATIONAL_B_SPLINE_CURVE ( ( 1.000000000000000000, 0.8047378541243663808, 0.8047378541243663808, 1.000000000000000000 ) ) 
 REPRESENTATION_ITEM ( '' )  );
#2416=CARTESIAN_POINT ( 'NONE',  ( 68.49370948373500312, 113.0390816101113387, 0.000000000000000000 ) ) ;
#2423=ORIENTED_EDGE ( 'NONE', *, *, #10266, .F. ) ;
#2425=CARTESIAN_POINT ( 'NONE',  ( 112.1804561881462945, 113.0390816101113387, 20.00000000000000000 ) ) ;
#2436=CYLINDRICAL_SURFACE ( 'NONE', #4341, 2.000000000000001776 ) ;
#2438=LINE ( 'NONE', #7967, #6491 ) ;
#2444=CARTESIAN_POINT ( 'NONE',  ( 50.53208251186094202, 104.0090514096174843, 23.00000000000000000 ) ) ;
#2449=EDGE_CURVE ( 'NONE', #878, #3128, #7599, .T. ) ;
#2456=ORIENTED_EDGE ( 'NONE', *, *, #3509, .T. ) ;
#2465=AXIS2_PLACEMENT_3D ( 'NONE', #4115, #11576, #6264 ) ;
#2471=CIRCLE ( 'NONE', #3800, 0.7499999999999966693 ) ;
#2476=CARTESIAN_POINT ( 'NONE',  ( 50.63563590245420443, 94.90549801902425031, 22.75000000000000000 ) ) ;
#2477=ADVANCED_FACE ( 'NONE', ( #8072 ), #4858, .T. ) ;
#2478=DIRECTION ( 'NONE',  ( 1.000000000000000000, 0.000000000000000000, 0.000000000000000000 ) ) ;
#2484=CARTESIAN_POINT ( 'NONE',  ( 142.6356359024541973, 111.0390816101113245, 19.25000000000000000 ) ) ;
#2486=ORIENTED_EDGE ( 'NONE', *, *, #7743, .F. ) ;
#2487=( BOUNDED_CURVE ( )  B_SPLINE_CURVE ( 3, ( #6116, #13465, #10329, #13393 ),
 .UNSPECIFIED., .F., .F. ) 
 B_SPLINE_CURVE_WITH_KNOTS ( ( 4, 4 ),
 ( 3.141592653589793116, 4.712388980384689674 ),
 .UNSPECIFIED. ) 
 CURVE ( )  GEOMETRIC_REPRESENTATION_ITEM ( )  RATIONAL_B_SPLINE_CURVE ( ( 1.000000000000000000, 0.8047378541243649375, 0.8047378541243649375, 1.000000000000000000 ) ) 
 REPRESENTATION_ITEM ( '' )  );
#2489=ORIENTED_EDGE ( 'NONE', *, *, #12363, .T. ) ;
#2495=DIRECTION ( 'NONE',  ( 1.000000000000000000, 0.000000000000000000, 0.000000000000000000 ) ) ;
#2503=ORIENTED_EDGE ( 'NONE', *, *, #9444, .F. ) ;
#2510=ORIENTED_EDGE ( 'NONE', *, *, #11140, .F. ) ;
#2512=VECTOR ( 'NONE', #9194, 1000.000000000000000 ) ;
#2515=FACE_BOUND ( 'NONE', #9741, .T. ) ;
#2520=VECTOR ( 'NONE', #404, 1000.000000000000000 ) ;
#2523=LINE ( 'NONE', #4462, #11168 ) ;
#2527=LINE ( 'NONE', #10187, #2864 ) ;
#2537=CARTESIAN_POINT ( 'NONE',  ( 68.49370948373500312, 75.03908161011133870, 0.7500000000000006661 ) ) ;
#2541=CARTESIAN_POINT ( 'NONE',  ( 42.63563590245419732, 111.0390816101113387, 0.7500000000000006661 ) ) ;
#2544=ORIENTED_EDGE ( 'NONE', *, *, #4528, .T. ) ;
#2563=ORIENTED_EDGE ( 'NONE', *, *, #2164, .T. ) ;
#2565=LINE ( 'NONE', #3459, #10125 ) ;
#2571=EDGE_CURVE ( 'NONE', #6531, #7944, #13712, .T. ) ;
#2578=DIRECTION ( 'NONE',  ( 1.000000000000000000, 0.000000000000000000, -0.000000000000000000 ) ) ;
#2582=ORIENTED_EDGE ( 'NONE', *, *, #12206, .T. ) ;
#2584=ORIENTED_EDGE ( 'NONE', *, *, #7199, .F. ) ;
#2585=EDGE_CURVE ( 'NONE', #6817, #13266, #4730, .T. ) ;
#2591=FACE_OUTER_BOUND ( 'NONE', #5203, .T. ) ;
#2594=CARTESIAN_POINT ( 'NONE',  ( 116.7775623211734342, 85.78908161011133870, 20.00000000000000000 ) ) ;
#2596=CARTESIAN_POINT ( 'NONE',  ( 50.63563590245420443, 108.9054980190242503, 20.00000000000000000 ) ) ;
#2600=DIRECTION ( 'NONE',  ( -0.000000000000000000, -0.000000000000000000, -1.000000000000000000 ) ) ;
#2602=PRODUCT_DEFINITION_SHAPE ( 'NONE', 'NONE',  #2207 ) ;
#2603=ORIENTED_EDGE ( 'NONE', *, *, #6983, .T. ) ;
#2610=LINE ( 'NONE', #11111, #3616 ) ;
#2613=LINE ( 'NONE', #8110, #5445 ) ;
#2621=AXIS2_PLACEMENT_3D ( 'NONE', #1837, #572, #9896 ) ;
#2622=ORIENTED_EDGE ( 'NONE', *, *, #2072, .F. ) ;
#2625=ORIENTED_EDGE ( 'NONE', *, *, #2404, .F. ) ;
#2631=EDGE_CURVE ( 'NONE', #6077, #10095, #2011, .T. ) ;
#2632=DIRECTION ( 'NONE',  ( 0.000000000000000000, 0.000000000000000000, 1.000000000000000000 ) ) ;
#2635=EDGE_CURVE ( 'NONE', #3128, #1998, #7368, .T. ) ;
#2636=VERTEX_POINT ( 'NONE', #1861 ) ;
#2647=AXIS2_PLACEMENT_3D ( 'NONE', #5748, #13093, #8982 ) ;
#2656=DIRECTION ( 'NONE',  ( -0.000000000000000000, -0.000000000000000000, -1.000000000000000000 ) ) ;
#2676=CIRCLE ( 'NONE', #11361, 2.000000000000001776 ) ;
#2681=CARTESIAN_POINT ( 'NONE',  ( 140.3249757306743675, 112.2890816101113387, 20.00000000000000000 ) ) ;
#2687=AXIS2_PLACEMENT_3D ( 'NONE', #8663, #7521, #3242 ) ;
#2691=( BOUNDED_CURVE ( )  B_SPLINE_CURVE ( 3, ( #8360, #12692, #9210, #3073 ),
 .UNSPECIFIED., .F., .F. ) 
 B_SPLINE_CURVE_WITH_KNOTS ( ( 4, 4 ),
 ( 1.570796326794896558, 3.141592653589793116 ),
 .UNSPECIFIED. ) 
 CURVE ( )  GEOMETRIC_REPRESENTATION_ITEM ( )  RATIONAL_B_SPLINE_CURVE ( ( 1.000000000000000000, 0.8047378541243649375, 0.8047378541243649375, 1.000000000000000000 ) ) 
 REPRESENTATION_ITEM ( '' )  );
#2692=ORIENTED_EDGE ( 'NONE', *, *, #11226, .F. ) ;
#2694=ORIENTED_EDGE ( 'NONE', *, *, #5908, .T. ) ;
#2695=EDGE_LOOP ( 'NONE', ( #6955, #7533 ) ) ;
#2697=VERTEX_POINT ( 'NONE', #3127 ) ;
#2699=PLANE ( 'NONE',  #13563 ) ;
#2701=PLANE ( 'NONE',  #11792 ) ;
#2712=EDGE_CURVE ( 'NONE', #11467, #878, #12318, .T. ) ;
#2724=VECTOR ( 'NONE', #6307, 1000.000000000000000 ) ;
#2738=CYLINDRICAL_SURFACE ( 'NONE', #5530, 0.2500000000000002220 ) ;
#2747=ORIENTED_EDGE ( 'NONE', *, *, #9742, .T. ) ;
#2752=EDGE_CURVE ( 'NONE', #1026, #5173, #268, .T. ) ;
#2761=DIRECTION ( 'NONE',  ( 1.000000000000000000, 0.000000000000000000, 0.000000000000000000 ) ) ;
#2762=AXIS2_PLACEMENT_3D ( 'NONE', #7423, #6466, #10733 ) ;
#2771=CARTESIAN_POINT ( 'NONE',  ( 134.6356359024541973, 89.90549801902423610, 22.75000000000000000 ) ) ;
#2773=DIRECTION ( 'NONE',  ( 0.000000000000000000, 1.000000000000000000, -0.000000000000000000 ) ) ;
#2779=VERTEX_POINT ( 'NONE', #11758 ) ;
#2786=CARTESIAN_POINT ( 'NONE',  ( 84.99521369064696330, 82.14063840035363739, 10.00000000000000000 ) ) ;
#2792=VECTOR ( 'NONE', #11678, 1000.000000000000000 ) ;
#2800=CARTESIAN_POINT ( 'NONE',  ( 140.6356359024541689, 85.03908161011133870, 19.25000000000000000 ) ) ;
#2803=CARTESIAN_POINT ( 'NONE',  ( 81.82136590429890077, 114.1051029460540605, 10.00000000000000000 ) ) ;
#2805=CARTESIAN_POINT ( 'NONE',  ( 50.63563590245420443, 108.6554980190242503, 22.75000000000000000 ) ) ;
#2807=CARTESIAN_POINT ( 'NONE',  ( 140.5320825118609207, 108.8019446284309737, 23.00000000000000000 ) ) ;
#2808=FACE_OUTER_BOUND ( 'NONE', #7830, .T. ) ;
#2809=EDGE_CURVE ( 'NONE', #3595, #6971, #12747, .T. ) ;
#2815=CARTESIAN_POINT ( 'NONE',  ( 140.6356359024541973, 85.03908161011132449, 0.3106601717798216367 ) ) ;
#2818=CARTESIAN_POINT ( 'NONE',  ( 92.63563590245421153, 99.03908161011133870, 20.00000000000000000 ) ) ;
#2828=ORIENTED_EDGE ( 'NONE', *, *, #112, .F. ) ;
#2835=DIRECTION ( 'NONE',  ( 0.000000000000000000, 1.000000000000000000, 0.000000000000000000 ) ) ;
#2837=DIRECTION ( 'NONE',  ( -0.000000000000000000, 1.000000000000000000, -0.000000000000000000 ) ) ;
#2840=AXIS2_PLACEMENT_3D ( 'NONE', #3895, #664, #6172 ) ;
#2841=DIRECTION ( 'NONE',  ( 0.000000000000000000, -1.000000000000000000, 0.000000000000000000 ) ) ;
#2844=ORIENTED_EDGE ( 'NONE', *, *, #6030, .F. ) ;
#2849=LINE ( 'NONE', #3812, #12228 ) ;
#2858=VERTEX_POINT ( 'NONE', #5668 ) ;
#2860=CARTESIAN_POINT ( 'NONE',  ( 50.63563590245420443, 89.90549801902423610, 22.75000000000000000 ) ) ;
#2864=VECTOR ( 'NONE', #604, 1000.000000000000000 ) ;
#2868=DIRECTION ( 'NONE',  ( 0.000000000000000000, 0.000000000000000000, 1.000000000000000000 ) ) ;
#2874=EDGE_LOOP ( 'NONE', ( #11378, #9881, #10391, #9389 ) ) ;
#2876=VERTEX_POINT ( 'NONE', #13155 ) ;
#2877=ORIENTED_EDGE ( 'NONE', *, *, #1052, .F. ) ;
#2878=DIRECTION ( 'NONE',  ( 1.000000000000000000, 0.000000000000000000, 0.000000000000000000 ) ) ;
#2888=DIRECTION ( 'NONE',  ( 0.000000000000000000, 0.000000000000000000, 1.000000000000000000 ) ) ;
#2889=FACE_OUTER_BOUND ( 'NONE', #4688, .T. ) ;
#2893=AXIS2_PLACEMENT_3D ( 'NONE', #7680, #9730, #11964 ) ;
#2895=EDGE_LOOP ( 'NONE', ( #6624, #15, #4647, #4108 ) ) ;
#2907=ORIENTED_EDGE ( 'NONE', *, *, #13701, .F. ) ;
#2908=FACE_OUTER_BOUND ( 'NONE', #13294, .T. ) ;
#2912=AXIS2_PLACEMENT_3D ( 'NONE', #10263, #7224, #4175 ) ;
#2916=ORIENTED_EDGE ( 'NONE', *, *, #1698, .F. ) ;
#2920=ORIENTED_EDGE ( 'NONE', *, *, #4571, .T. ) ;
#2926=CARTESIAN_POINT ( 'NONE',  ( 134.6356359024541973, 103.9054980190242361, 23.00000000000000000 ) ) ;
#2938=DIRECTION ( 'NONE',  ( 0.000000000000000000, -1.000000000000000000, 0.000000000000000000 ) ) ;
#2940=AXIS2_PLACEMENT_3D ( 'NONE', #10100, #12390, #715 ) ;
#2942=FACE_OUTER_BOUND ( 'NONE', #13551, .T. ) ;
#2943=AXIS2_PLACEMENT_3D ( 'NONE', #4912, #2773, #1842 ) ;
#2945=DIRECTION ( 'NONE',  ( 0.7091883091770476710, -0.7050191076322684935, 0.000000000000000000 ) ) ;
#2952=VERTEX_POINT ( 'NONE', #5881 ) ;
#2955=EDGE_LOOP ( 'NONE', ( #11393, #1974, #8040, #8349 ) ) ;
#2956=ORIENTED_EDGE ( 'NONE', *, *, #61, .F. ) ;
#2957=ORIENTED_EDGE ( 'NONE', *, *, #3611, .T. ) ;
#2959=DIRECTION ( 'NONE',  ( 0.000000000000000000, -1.000000000000000000, 0.000000000000000000 ) ) ;
#2962=VECTOR ( 'NONE', #13332, 1000.000000000000000 ) ;
#2972=VERTEX_POINT ( 'NONE', #713 ) ;
#2980=ORIENTED_EDGE ( 'NONE', *, *, #6977, .T. ) ;
#2982=DIRECTION ( 'NONE',  ( 0.000000000000000000, 0.000000000000000000, 1.000000000000000000 ) ) ;
#2988=ORIENTED_EDGE ( 'NONE', *, *, #2309, .F. ) ;
#2989=VECTOR ( 'NONE', #11354, 1000.000000000000000 ) ;
#2993=ORIENTED_EDGE ( 'NONE', *, *, #12512, .F. ) ;
#2995=DIRECTION ( 'NONE',  ( -0.000000000000000000, -0.000000000000000000, 1.000000000000000000 ) ) ;
#2996=DIRECTION ( 'NONE',  ( 1.000000000000000000, -0.000000000000000000, 0.000000000000000000 ) ) ;
#2998=FACE_BOUND ( 'NONE', #2276, .T. ) ;
#3007=DIRECTION ( 'NONE',  ( 0.000000000000000000, -0.000000000000000000, -1.000000000000000000 ) ) ;
#3015=CARTESIAN_POINT ( 'NONE',  ( 50.63563590245420443, 103.9054980190242361, 20.00000000000000000 ) ) ;
#3020=ORIENTED_EDGE ( 'NONE', *, *, #7468, .T. ) ;
#3028=LINE ( 'NONE', #2107, #8280 ) ;
#3034=ORIENTED_EDGE ( 'NONE', *, *, #8529, .T. ) ;
#3039=EDGE_LOOP ( 'NONE', ( #3401, #1357, #4355, #2035 ) ) ;
#3040=CARTESIAN_POINT ( 'NONE',  ( 44.94629607423406270, 112.2890816101113387, 20.00000000000000000 ) ) ;
#3050=ORIENTED_EDGE ( 'NONE', *, *, #8509, .T. ) ;
#3052=ORIENTED_EDGE ( 'NONE', *, *, #12850, .T. ) ;
#3057=DIRECTION ( 'NONE',  ( 0.000000000000000000, 0.000000000000000000, 1.000000000000000000 ) ) ;
#3063=EDGE_CURVE ( 'NONE', #12738, #12630, #10930, .T. ) ;
#3065=VECTOR ( 'NONE', #1492, 1000.000000000000000 ) ;
#3066=CARTESIAN_POINT ( 'NONE',  ( 140.6356359024541973, 113.0390816101113387, 19.25000000000000000 ) ) ;
#3072=LINE ( 'NONE', #3140, #2310 ) ;
#3073=CARTESIAN_POINT ( 'NONE',  ( 44.63563590245420443, 103.9054980190242361, 22.75000000000000000 ) ) ;
#3077=CIRCLE ( 'NONE', #10199, 2.000000000000001776 ) ;
#3092=EDGE_CURVE ( 'NONE', #12738, #4329, #3298, .T. ) ;
#3098=DIRECTION ( 'NONE',  ( 0.000000000000000000, 0.000000000000000000, -1.000000000000000000 ) ) ;
#3103=CARTESIAN_POINT ( 'NONE',  ( 109.1537879975201406, 115.4601262030644762, 19.25000000000000000 ) ) ;
#3105=DIRECTION ( 'NONE',  ( 0.000000000000000000, 0.000000000000000000, 1.000000000000000000 ) ) ;
#3107=LINE ( 'NONE', #7330, #2724 ) ;
#3109=AXIS2_PLACEMENT_3D ( 'NONE', #12864, #85, #6579 ) ;
#3114=ORIENTED_EDGE ( 'NONE', *, *, #299, .T. ) ;
#3119=AXIS2_PLACEMENT_3D ( 'NONE', #10208, #7952, #4897 ) ;
#3122=CARTESIAN_POINT ( 'NONE',  ( 42.63563590245419732, 87.03908161011136713, 19.25000000000000000 ) ) ;
#3124=LINE ( 'NONE', #89, #5157 ) ;
#3127=CARTESIAN_POINT ( 'NONE',  ( 68.49370948373500312, 85.78908161011133870, 20.00000000000000000 ) ) ;
#3128=VERTEX_POINT ( 'NONE', #5307 ) ;
#3133=ADVANCED_FACE ( 'NONE', ( #212 ), #3184, .T. ) ;
#3134=DIRECTION ( 'NONE',  ( -0.000000000000000000, -0.000000000000000000, -1.000000000000000000 ) ) ;
#3140=CARTESIAN_POINT ( 'NONE',  ( 140.6356359024541973, 104.1554980190242361, 23.00000000000000000 ) ) ;
#3144=DIRECTION ( 'NONE',  ( 1.000000000000000000, 0.000000000000000000, 0.000000000000000000 ) ) ;
#3146=EDGE_CURVE ( 'NONE', #1109, #11822, #7394, .T. ) ;
#3159=LINE ( 'NONE', #6128, #18 ) ;
#3160=CARTESIAN_POINT ( 'NONE',  ( 76.11748380738829667, 115.4601262030644762, 20.00000000000000000 ) ) ;
#3163=DIRECTION ( 'NONE',  ( -0.000000000000000000, -0.000000000000000000, 1.000000000000000000 ) ) ;
#3173=ORIENTED_EDGE ( 'NONE', *, *, #8156, .T. ) ;
#3184=PLANE ( 'NONE',  #2687 ) ;
#3193=VERTEX_POINT ( 'NONE', #6366 ) ;
#3194=ADVANCED_FACE ( 'NONE', ( #9656 ), #2192, .T. ) ;
#3196=ADVANCED_FACE ( 'NONE', ( #12920 ), #11887, .F. ) ;
#3198=DIRECTION ( 'NONE',  ( 1.000000000000000000, -0.000000000000000000, 0.000000000000000000 ) ) ;
#3208=PLANE ( 'NONE',  #4680 ) ;
#3210=DIRECTION ( 'NONE',  ( -0.7071067811865451302, 0.7071067811865500152, -0.000000000000000000 ) ) ;
#3211=AXIS2_PLACEMENT_3D ( 'NONE', #3669, #2632, #8124 ) ;
#3218=ORIENTED_EDGE ( 'NONE', *, *, #11649, .F. ) ;
#3225=EDGE_CURVE ( 'NONE', #4904, #6817, #1469, .T. ) ;
#3229=EDGE_CURVE ( 'NONE', #2636, #1997, #10001, .T. ) ;
#3232=ORIENTED_EDGE ( 'NONE', *, *, #7998, .F. ) ;
#3237=CARTESIAN_POINT ( 'NONE',  ( 134.6356359024541973, 94.90549801902425031, 23.00000000000000000 ) ) ;
#3241=LINE ( 'NONE', #13695, #10463 ) ;
#3242=DIRECTION ( 'NONE',  ( 0.000000000000000000, 0.000000000000000000, 1.000000000000000000 ) ) ;
#3250=ORIENTED_EDGE ( 'NONE', *, *, #13229, .T. ) ;
#3251=ORIENTED_EDGE ( 'NONE', *, *, #7468, .F. ) ;
#3253=DIRECTION ( 'NONE',  ( 0.000000000000000000, 0.000000000000000000, -1.000000000000000000 ) ) ;
#3255=CARTESIAN_POINT ( 'NONE',  ( 44.63563590245419732, 94.90549801902423610, 22.89644660940672694 ) ) ;
#3260=CARTESIAN_POINT ( 'NONE',  ( 142.6356359024541973, 87.03908161011133870, 19.25000000000000000 ) ) ;
#3262=ADVANCED_FACE ( 'NONE', ( #8955 ), #5587, .T. ) ;
#3264=EDGE_LOOP ( 'NONE', ( #9306, #10844, #10140, #12147 ) ) ;
#3268=DIRECTION ( 'NONE',  ( 0.000000000000000000, 1.000000000000000000, 0.000000000000000000 ) ) ;
#3274=DIRECTION ( 'NONE',  ( 0.000000000000000000, 0.000000000000000000, 1.000000000000000000 ) ) ;
#3275=CARTESIAN_POINT ( 'NONE',  ( 140.5069562460138286, 85.34974178189114014, 20.00000000000000000 ) ) ;
#3277=AXIS2_PLACEMENT_3D ( 'NONE', #8415, #11641, #1015 ) ;
#3278=CYLINDRICAL_SURFACE ( 'NONE', #7241, 0.7500000000000006661 ) ;
#3279=EDGE_CURVE ( 'NONE', #3533, #5517, #7889, .T. ) ;
#3284=DIRECTION ( 'NONE',  ( -1.000000000000000000, 0.000000000000000000, 0.000000000000000000 ) ) ;
#3294=CYLINDRICAL_SURFACE ( 'NONE', #682, 0.2500000000000002220 ) ;
#3295=DIRECTION ( 'NONE',  ( -0.000000000000000000, -0.000000000000000000, -1.000000000000000000 ) ) ;
#3298=LINE ( 'NONE', #7602, #3338 ) ;
#3308=CARTESIAN_POINT ( 'NONE',  ( 68.49370948373500312, 113.0390816101113387, 19.25000000000000000 ) ) ;
#3309=DIRECTION ( 'NONE',  ( 0.000000000000000000, 0.000000000000000000, -1.000000000000000000 ) ) ;
#3312=VECTOR ( 'NONE', #5291, 1000.000000000000114 ) ;
#3317=DIRECTION ( 'NONE',  ( -0.000000000000000000, -0.000000000000000000, -1.000000000000000000 ) ) ;
#3320=FACE_OUTER_BOUND ( 'NONE', #2402, .T. ) ;
#3323=ORIENTED_EDGE ( 'NONE', *, *, #6326, .F. ) ;
#3328=DIRECTION ( 'NONE',  ( 1.000000000000000000, 0.000000000000000000, 0.000000000000000000 ) ) ;
#3330=DIRECTION ( 'NONE',  ( 1.000000000000000000, 0.000000000000000000, 0.000000000000000000 ) ) ;
#3332=CARTESIAN_POINT ( 'NONE',  ( 44.63563590245421864, 85.03908161011133870, 0.7500000000000006661 ) ) ;
#3335=ADVANCED_FACE ( 'NONE', ( #2889 ), #9230, .F. ) ;
#3338=VECTOR ( 'NONE', #1049, 1000.000000000000000 ) ;
#3342=CARTESIAN_POINT ( 'NONE',  ( 92.63563590245421153, 85.78908161011133870, 19.25000000000000000 ) ) ;
#3348=CARTESIAN_POINT ( 'NONE',  ( 92.63563590245421153, 99.03908161011133870, -30.00000000000001776 ) ) ;
#3349=VECTOR ( 'NONE', #1444, 1000.000000000000000 ) ;
#3358=CIRCLE ( 'NONE', #12045, 2.000000000000001776 ) ;
#3359=AXIS2_PLACEMENT_3D ( 'NONE', #8802, #13131, #4347 ) ;
#3361=ORIENTED_EDGE ( 'NONE', *, *, #12048, .F. ) ;
#3367=DIRECTION ( 'NONE',  ( -1.000000000000000000, 0.000000000000000000, 0.000000000000000000 ) ) ;
#3368=ORIENTED_EDGE ( 'NONE', *, *, #2712, .T. ) ;
#3369=CARTESIAN_POINT ( 'NONE',  ( 42.63563590245419732, 85.03908161011133870, 0.7500000000000006661 ) ) ;
#3370=DIRECTION ( 'NONE',  ( -1.000000000000000000, -0.000000000000000000, 0.000000000000000000 ) ) ;
#3381=DIRECTION ( 'NONE',  ( -0.7071067811865520136, 0.7071067811865429098, 0.000000000000000000 ) ) ;
#3386=ORIENTED_EDGE ( 'NONE', *, *, #3279, .T. ) ;
#3388=FACE_OUTER_BOUND ( 'NONE', #10319, .T. ) ;
#3392=DIRECTION ( 'NONE',  ( 0.000000000000000000, 0.000000000000000000, 1.000000000000000000 ) ) ;
#3399=ADVANCED_FACE ( 'NONE', ( #9158 ), #10343, .T. ) ;
#3401=ORIENTED_EDGE ( 'NONE', *, *, #7558, .T. ) ;
#3404=CARTESIAN_POINT ( 'NONE',  ( 134.8856359024541973, 90.15549801902423610, 23.00000000000000000 ) ) ;
#3415=AXIS2_PLACEMENT_3D ( 'NONE', #6746, #13168, #9749 ) ;
#3418=EDGE_CURVE ( 'NONE', #12860, #135, #7181, .T. ) ;
#3422=LINE ( 'NONE', #11030, #8266 ) ;
#3423=DIRECTION ( 'NONE',  ( 0.000000000000000000, 0.000000000000000000, 1.000000000000000000 ) ) ;
#3428=VERTEX_POINT ( 'NONE', #830 ) ;
#3429=CARTESIAN_POINT ( 'NONE',  ( 142.6356359024541973, 111.0390816101113245, 19.25000000000000000 ) ) ;
#3430=CARTESIAN_POINT ( 'NONE',  ( 92.63563590245421153, 99.03908161011133870, 0.7500000000000006661 ) ) ;
#3435=EDGE_LOOP ( 'NONE', ( #3848, #2692, #933, #1817 ) ) ;
#3442=PLANE ( 'NONE',  #4890 ) ;
#3443=CIRCLE ( 'NONE', #12792, 2.000000000000001776 ) ;
#3445=CARTESIAN_POINT ( 'NONE',  ( 74.18094369249178044, 97.20665973629650125, 10.00000000000000000 ) ) ;
#3450=ORIENTED_EDGE ( 'NONE', *, *, #6475, .F. ) ;
#3454=PLANE ( 'NONE',  #10436 ) ;
#3456=DIRECTION ( 'NONE',  ( 0.000000000000000000, 1.000000000000000000, -0.000000000000000000 ) ) ;
#3459=CARTESIAN_POINT ( 'NONE',  ( 134.6356359024541973, 89.90549801902423610, 23.00000000000000000 ) ) ;
#3460=DIRECTION ( 'NONE',  ( 1.000000000000000000, 0.000000000000000000, 0.000000000000000000 ) ) ;
#3487=FACE_OUTER_BOUND ( 'NONE', #395, .T. ) ;
#3494=AXIS2_PLACEMENT_3D ( 'NONE', #12476, #13514, #12615 ) ;
#3496=DIRECTION ( 'NONE',  ( 1.000000000000000000, 0.000000000000000000, -0.000000000000000000 ) ) ;
#3505=CARTESIAN_POINT ( 'NONE',  ( 112.1804561881462945, 85.78908161011133870, 0.7500000000000006661 ) ) ;
#3509=EDGE_CURVE ( 'NONE', #9587, #8944, #3358, .T. ) ;
#3512=VERTEX_POINT ( 'NONE', #1585 ) ;
#3519=EDGE_LOOP ( 'NONE', ( #10606, #5170, #10765, #6921 ) ) ;
#3521=CARTESIAN_POINT ( 'NONE',  ( 134.6356359024541973, 108.9054980190242503, 20.00000000000000000 ) ) ;
#3524=CARTESIAN_POINT ( 'NONE',  ( 68.49370948373500312, 75.03908161011133870, 19.25000000000000000 ) ) ;
#3528=VECTOR ( 'NONE', #728, 1000.000000000000000 ) ;
#3531=EDGE_CURVE ( 'NONE', #4189, #3713, #6014, .T. ) ;
#3533=VERTEX_POINT ( 'NONE', #10049 ) ;
#3535=ORIENTED_EDGE ( 'NONE', *, *, #9694, .F. ) ;
#3543=VERTEX_POINT ( 'NONE', #12140 ) ;
#3544=DIRECTION ( 'NONE',  ( 1.000000000000000000, 0.000000000000000000, 0.000000000000000000 ) ) ;
#3551=CIRCLE ( 'NONE', #3109, 2.000000000000001776 ) ;
#3553=EDGE_CURVE ( 'NONE', #8944, #1263, #1381, .T. ) ;
#3567=CIRCLE ( 'NONE', #7313, 0.7500000000000006661 ) ;
#3573=ADVANCED_FACE ( 'NONE', ( #12202 ), #1103, .T. ) ;
#3577=ORIENTED_EDGE ( 'NONE', *, *, #11226, .T. ) ;
#3580=LINE ( 'NONE', #13329, #140 ) ;
#3584=CARTESIAN_POINT ( 'NONE',  ( 92.63563590245421153, 99.03908161011133870, 0.7500000000000006661 ) ) ;
#3586=LINE ( 'NONE', #7819, #674 ) ;
#3595=VERTEX_POINT ( 'NONE', #1651 ) ;
#3601=ORIENTED_EDGE ( 'NONE', *, *, #10615, .F. ) ;
#3602=FACE_OUTER_BOUND ( 'NONE', #839, .T. ) ;
#3603=CARTESIAN_POINT ( 'NONE',  ( 134.8856359024541973, 108.6554980190242503, 23.00000000000000000 ) ) ;
#3605=CARTESIAN_POINT ( 'NONE',  ( 68.49370948373500312, 75.03908161011133870, 0.7500000000000006661 ) ) ;
#3610=VERTEX_POINT ( 'NONE', #7788 ) ;
#3611=EDGE_CURVE ( 'NONE', #8025, #1567, #2523, .T. ) ;
#3613=VERTEX_POINT ( 'NONE', #10051 ) ;
#3616=VECTOR ( 'NONE', #4618, 1000.000000000000000 ) ;
#3631=DIRECTION ( 'NONE',  ( 1.000000000000000000, -0.000000000000000000, 0.000000000000000000 ) ) ;
#3633=DIRECTION ( 'NONE',  ( 0.7071067811865500152, 0.7071067811865451302, 0.000000000000000000 ) ) ;
#3643=CARTESIAN_POINT ( 'NONE',  ( 44.94629607423406270, 112.2890816101113387, 0.000000000000000000 ) ) ;
#3644=VECTOR ( 'NONE', #13772, 1000.000000000000000 ) ;
#3646=ORIENTED_EDGE ( 'NONE', *, *, #8395, .T. ) ;
#3648=DIRECTION ( 'NONE',  ( 0.000000000000000000, 0.000000000000000000, 1.000000000000000000 ) ) ;
#3649=DIRECTION ( 'NONE',  ( 0.000000000000000000, 0.000000000000000000, 1.000000000000000000 ) ) ;
#3652=EDGE_CURVE ( 'NONE', #1569, #3713, #9853, .T. ) ;
#3653=CARTESIAN_POINT ( 'NONE',  ( 141.8856359024541973, 99.03908161011133870, 19.25000000000000000 ) ) ;
#3654=FACE_OUTER_BOUND ( 'NONE', #11397, .T. ) ;
#3656=EDGE_CURVE ( 'NONE', #9517, #1552, #3422, .T. ) ;
#3661=ORIENTED_EDGE ( 'NONE', *, *, #11608, .T. ) ;
#3662=AXIS2_PLACEMENT_3D ( 'NONE', #7027, #8152, #13594 ) ;
#3665=CARTESIAN_POINT ( 'NONE',  ( 141.8856359024541973, 111.0390816101113103, 20.00000000000000000 ) ) ;
#3669=CARTESIAN_POINT ( 'NONE',  ( 103.4499059006094512, 83.97306027416853169, 20.00000000000000000 ) ) ;
#3676=CARTESIAN_POINT ( 'NONE',  ( 44.63563590245420443, 108.9054980190242503, 22.75000000000000000 ) ) ;
#3680=CARTESIAN_POINT ( 'NONE',  ( 140.1053058165642824, 85.56941169600125363, 0.000000000000000000 ) ) ;
#3685=EDGE_CURVE ( 'NONE', #9992, #5932, #13184, .T. ) ;
#3691=DIRECTION ( 'NONE',  ( -0.7071067811865451302, 0.7071067811865500152, 0.000000000000000000 ) ) ;
#3692=CYLINDRICAL_SURFACE ( 'NONE', #9642, 0.7500000000000000000 ) ;
#3700=ORIENTED_EDGE ( 'NONE', *, *, #9319, .T. ) ;
#3708=DIRECTION ( 'NONE',  ( 0.000000000000000000, 0.000000000000000000, -1.000000000000000000 ) ) ;
#3713=VERTEX_POINT ( 'NONE', #4595 ) ;
#3718=ORIENTED_EDGE ( 'NONE', *, *, #10632, .F. ) ;
#3730=( BOUNDED_CURVE ( )  B_SPLINE_CURVE ( 3, ( #11774, #9547, #9690, #106 ),
 .UNSPECIFIED., .F., .F. ) 
 B_SPLINE_CURVE_WITH_KNOTS ( ( 4, 4 ),
 ( 0.000000000000000000, 1.570796326794896558 ),
 .UNSPECIFIED. ) 
 CURVE ( )  GEOMETRIC_REPRESENTATION_ITEM ( )  RATIONAL_B_SPLINE_CURVE ( ( 1.000000000000000000, 0.8047378541243649375, 0.8047378541243649375, 1.000000000000000000 ) ) 
 REPRESENTATION_ITEM ( '' )  );
#3735=EDGE_LOOP ( 'NONE', ( #5057, #856, #207, #21 ) ) ;
#3736=DIRECTION ( 'NONE',  ( 0.000000000000000000, 0.000000000000000000, 1.000000000000000000 ) ) ;
#3737=ORIENTED_EDGE ( 'NONE', *, *, #12767, .F. ) ;
#3739=EDGE_CURVE ( 'NONE', #10924, #2221, #5484, .T. ) ;
#3741=VECTOR ( 'NONE', #2996, 1000.000000000000000 ) ;
#3743=CARTESIAN_POINT ( 'NONE',  ( 50.63563590245420443, 103.9054980190242361, 22.89644660940672694 ) ) ;
#3746=VECTOR ( 'NONE', #6669, 1000.000000000000000 ) ;
#3750=AXIS2_PLACEMENT_3D ( 'NONE', #1612, #3392, #3460 ) ;
#3752=VECTOR ( 'NONE', #3456, 1000.000000000000000 ) ;
#3765=PLANE ( 'NONE',  #5420 ) ;
#3767=CIRCLE ( 'NONE', #3750, 10.74999999999999645 ) ;
#3775=VERTEX_POINT ( 'NONE', #7161 ) ;
#3776=CARTESIAN_POINT ( 'NONE',  ( 75.58559257550551536, 82.08927268643400055, 20.00000000000000000 ) ) ;
#3777=TOROIDAL_SURFACE ( 'NONE', #2465, 10.75000000000000000, 0.7500000000000000000 ) ;
#3778=ADVANCED_FACE ( 'NONE', ( #7019 ), #7803, .T. ) ;
#3792=DIRECTION ( 'NONE',  ( 0.000000000000000000, 0.000000000000000000, 1.000000000000000000 ) ) ;
#3800=AXIS2_PLACEMENT_3D ( 'NONE', #9404, #4927, #5055 ) ;
#3803=EDGE_CURVE ( 'NONE', #7944, #4071, #5900, .T. ) ;
#3806=CIRCLE ( 'NONE', #3359, 0.7499999999999966693 ) ;
#3808=TOROIDAL_SURFACE ( 'NONE', #4710, 23.29163056034262169, 0.7500000000000000000 ) ;
#3812=CARTESIAN_POINT ( 'NONE',  ( 142.6356359024541973, 87.03908161011133870, 19.25000000000000000 ) ) ;
#3821=( BOUNDED_CURVE ( )  B_SPLINE_CURVE ( 3, ( #4320, #12763, #3275, #4452 ),
 .UNSPECIFIED., .F., .F. ) 
 B_SPLINE_CURVE_WITH_KNOTS ( ( 4, 4 ),
 ( 0.000000000000000000, 1.570796326794896558 ),
 .UNSPECIFIED. ) 
 CURVE ( )  GEOMETRIC_REPRESENTATION_ITEM ( )  RATIONAL_B_SPLINE_CURVE ( ( 1.000000000000000000, 0.8047378541243649375, 0.8047378541243649375, 1.000000000000000000 ) ) 
 REPRESENTATION_ITEM ( '' )  );
#3822=AXIS2_PLACEMENT_3D ( 'NONE', #4464, #3284, #119 ) ;
#3828=DIRECTION ( 'NONE',  ( -1.000000000000000000, 0.000000000000000000, 0.000000000000000000 ) ) ;
#3829=VECTOR ( 'NONE', #10261, 1000.000000000000000 ) ;
#3837=CARTESIAN_POINT ( 'NONE',  ( 123.1053058165644671, 129.5087515242213669, 20.00000000000000000 ) ) ;
#3840=CYLINDRICAL_SURFACE ( 'NONE', #11, 0.2500000000000002220 ) ;
#3844=VECTOR ( 'NONE', #12900, 1000.000000000000000 ) ;
#3848=ORIENTED_EDGE ( 'NONE', *, *, #8265, .T. ) ;
#3855=CARTESIAN_POINT ( 'NONE',  ( 75.58559257550551536, 82.08927268643400055, 19.25000000000000000 ) ) ;
#3865=ORIENTED_EDGE ( 'NONE', *, *, #10743, .F. ) ;
#3866=ORIENTED_EDGE ( 'NONE', *, *, #10802, .T. ) ;
#3869=ORIENTED_EDGE ( 'NONE', *, *, #5166, .F. ) ;
#3873=DIRECTION ( 'NONE',  ( 0.7071067811865382469, -0.7071067811865567876, 0.000000000000000000 ) ) ;
#3876=DIRECTION ( 'NONE',  ( -0.000000000000000000, -0.000000000000000000, -1.000000000000000000 ) ) ;
#3882=ORIENTED_EDGE ( 'NONE', *, *, #3656, .F. ) ;
#3886=ORIENTED_EDGE ( 'NONE', *, *, #2363, .F. ) ;
#3887=DIRECTION ( 'NONE',  ( 0.000000000000000000, 0.000000000000000000, 1.000000000000000000 ) ) ;
#3889=FACE_OUTER_BOUND ( 'NONE', #618, .T. ) ;
#3891=ORIENTED_EDGE ( 'NONE', *, *, #7820, .T. ) ;
#3895=CARTESIAN_POINT ( 'NONE',  ( 68.49370948373500312, 123.0390816101113245, 20.00000000000000000 ) ) ;
#3897=ORIENTED_EDGE ( 'NONE', *, *, #13123, .T. ) ;
#3902=( BOUNDED_CURVE ( )  B_SPLINE_CURVE ( 3, ( #2484, #4419, #12031, #7675 ),
 .UNSPECIFIED., .F., .T. ) 
 B_SPLINE_CURVE_WITH_KNOTS ( ( 4, 4 ),
 ( 0.000000000000000000, 1.570796326794890119 ),
 .UNSPECIFIED. ) 
 CURVE ( )  GEOMETRIC_REPRESENTATION_ITEM ( )  RATIONAL_B_SPLINE_CURVE ( ( 1.000000000000000000, 0.8047378541243663808, 0.8047378541243663808, 1.000000000000000000 ) ) 
 REPRESENTATION_ITEM ( '' )  );
#3904=CARTESIAN_POINT ( 'NONE',  ( 44.88563590245420443, 0.000000000000000000, 23.00000000000000000 ) ) ;
#3909=ORIENTED_EDGE ( 'NONE', *, *, #7266, .T. ) ;
#3912=CARTESIAN_POINT ( 'NONE',  ( 44.63563590245420443, 94.90549801902425031, 20.00000000000000000 ) ) ;
#3913=EDGE_LOOP ( 'NONE', ( #5388, #11661, #2510, #522 ) ) ;
#3915=DIRECTION ( 'NONE',  ( 0.000000000000000000, 0.000000000000000000, 1.000000000000000000 ) ) ;
#3916=DIRECTION ( 'NONE',  ( -1.000000000000000000, 0.000000000000000000, 0.000000000000000000 ) ) ;
#3920=CARTESIAN_POINT ( 'NONE',  ( 44.63563590245421864, 85.03908161011133870, 19.25000000000000000 ) ) ;
#3922=FACE_OUTER_BOUND ( 'NONE', #9427, .T. ) ;
#3930=CARTESIAN_POINT ( 'NONE',  ( 100.2760581142613603, 115.9375248198690826, 10.00000000000000000 ) ) ;
#3939=CIRCLE ( 'NONE', #6137, 6.000000000000005329 ) ;
#3941=VERTEX_POINT ( 'NONE', #1084 ) ;
#3944=ORIENTED_EDGE ( 'NONE', *, *, #8975, .T. ) ;
#3947=FACE_OUTER_BOUND ( 'NONE', #6566, .T. ) ;
#3952=DIRECTION ( 'NONE',  ( -0.000000000000000000, -0.000000000000000000, -1.000000000000000000 ) ) ;
#3957=FACE_OUTER_BOUND ( 'NONE', #2229, .T. ) ;
#3961=LINE ( 'NONE', #8355, #147 ) ;
#3962=DIRECTION ( 'NONE',  ( 0.000000000000000000, 1.000000000000000000, -0.000000000000000000 ) ) ;
#3964=CARTESIAN_POINT ( 'NONE',  ( 134.6356359024541973, 89.90549801902423610, 22.89644660940672694 ) ) ;
#3980=VERTEX_POINT ( 'NONE', #6175 ) ;
#3986=DIRECTION ( 'NONE',  ( 0.000000000000000000, -1.000000000000000000, 0.000000000000000000 ) ) ;
#3990=EDGE_CURVE ( 'NONE', #11751, #13530, #12934, .T. ) ;
#3992=ADVANCED_FACE ( 'NONE', ( #6463 ), #4313, .T. ) ;
#4002=CARTESIAN_POINT ( 'NONE',  ( 141.8856359024541973, 99.03908161011133870, 0.000000000000000000 ) ) ;
#4004=LINE ( 'NONE', #6142, #7589 ) ;
#4006=FACE_OUTER_BOUND ( 'NONE', #5851, .T. ) ;
#4012=LINE ( 'NONE', #13358, #6250 ) ;
#4016=ADVANCED_FACE ( 'NONE', ( #2224 ), #8554, .T. ) ;
#4022=ORIENTED_EDGE ( 'NONE', *, *, #9485, .T. ) ;
#4036=ORIENTED_EDGE ( 'NONE', *, *, #10743, .T. ) ;
#4044=DIRECTION ( 'NONE',  ( 0.000000000000000000, 0.000000000000000000, 1.000000000000000000 ) ) ;
#4059=ORIENTED_EDGE ( 'NONE', *, *, #4182, .T. ) ;
#4062=ORIENTED_EDGE ( 'NONE', *, *, #4182, .F. ) ;
#4065=LINE ( 'NONE', #11315, #13411 ) ;
#4066=DIRECTION ( 'NONE',  ( 1.000000000000000000, 0.000000000000000000, 0.000000000000000000 ) ) ;
#4071=VERTEX_POINT ( 'NONE', #4109 ) ;
#4077=DIRECTION ( 'NONE',  ( 0.000000000000000000, 0.000000000000000000, 1.000000000000000000 ) ) ;
#4085=DIRECTION ( 'NONE',  ( 1.000000000000000000, 1.387778780781446464E-15, 0.000000000000000000 ) ) ;
#4090=EDGE_CURVE ( 'NONE', #10605, #2697, #13179, .T. ) ;
#4093=EDGE_LOOP ( 'NONE', ( #8233, #287, #862, #6235 ) ) ;
#4096=CARTESIAN_POINT ( 'NONE',  ( 50.63563590245420443, 108.9054980190242503, 23.00000000000000000 ) ) ;
#4098=CARTESIAN_POINT ( 'NONE',  ( 92.63563590245421153, 99.03908161011133870, 0.7500000000000006661 ) ) ;
#4102=ORIENTED_EDGE ( 'NONE', *, *, #8509, .F. ) ;
#4106=DIRECTION ( 'NONE',  ( 0.000000000000000000, 1.000000000000000000, 0.000000000000000000 ) ) ;
#4107=ORIENTED_EDGE ( 'NONE', *, *, #13109, .T. ) ;
#4108=ORIENTED_EDGE ( 'NONE', *, *, #2585, .T. ) ;
#4109=CARTESIAN_POINT ( 'NONE',  ( 50.63563590245420443, 94.90549801902425031, 20.00000000000000000 ) ) ;
#4110=CARTESIAN_POINT ( 'NONE',  ( 50.63563590245420443, 103.9054980190242361, 23.00000000000000000 ) ) ;
#4115=CARTESIAN_POINT ( 'NONE',  ( 116.7775623211734342, 123.0390816101113245, 0.7500000000000006661 ) ) ;
#4120=ORIENTED_EDGE ( 'NONE', *, *, #6239, .F. ) ;
#4124=ORIENTED_EDGE ( 'NONE', *, *, #730, .F. ) ;
#4128=CARTESIAN_POINT ( 'NONE',  ( 134.8856359024541973, 108.6554980190242503, 23.00000000000000000 ) ) ;
#4131=ORIENTED_EDGE ( 'NONE', *, *, #2124, .F. ) ;
#4133=ORIENTED_EDGE ( 'NONE', *, *, #13123, .F. ) ;
#4137=LINE ( 'NONE', #3237, #2792 ) ;
#4150=VERTEX_POINT ( 'NONE', #11266 ) ;
#4152=DIRECTION ( 'NONE',  ( 0.000000000000000000, 0.000000000000000000, 1.000000000000000000 ) ) ;
#4162=EDGE_CURVE ( 'NONE', #6593, #1954, #2438, .T. ) ;
#4165=EDGE_CURVE ( 'NONE', #1026, #8282, #11618, .T. ) ;
#4170=VERTEX_POINT ( 'NONE', #4833 ) ;
#4172=DIRECTION ( 'NONE',  ( 0.7071067811865524577, 0.7071067811865425767, -0.000000000000000000 ) ) ;
#4173=FACE_OUTER_BOUND ( 'NONE', #2116, .T. ) ;
#4175=DIRECTION ( 'NONE',  ( -0.000000000000000000, 0.000000000000000000, -1.000000000000000000 ) ) ;
#4176=CARTESIAN_POINT ( 'NONE',  ( 75.58559257550551536, 115.9888905337886769, 0.7500000000000006661 ) ) ;
#4177=CARTESIAN_POINT ( 'NONE',  ( 76.11748380738829667, 115.4601262030644762, 19.25000000000000000 ) ) ;
#4182=EDGE_CURVE ( 'NONE', #1263, #10693, #10963, .T. ) ;
#4186=CARTESIAN_POINT ( 'NONE',  ( 140.3856359024541973, 94.65549801902425031, 23.00000000000000000 ) ) ;
#4189=VERTEX_POINT ( 'NONE', #10291 ) ;
#4193=CARTESIAN_POINT ( 'NONE',  ( 84.99521369064696330, 82.14063840035363739, 20.00000000000000000 ) ) ;
#4194=LINE ( 'NONE', #5490, #5300 ) ;
#4195=CARTESIAN_POINT ( 'NONE',  ( 98.63563590245422574, 99.03908161011133870, -30.00000000000001776 ) ) ;
#4198=MECHANICAL_DESIGN_GEOMETRIC_PRESENTATION_REPRESENTATION('',(#6415),#4640);
#4202=AXIS2_PLACEMENT_3D ( 'NONE', #5571, #9861, #3496 ) ;
#4205=EDGE_LOOP ( 'NONE', ( #12975, #706, #2582, #8461 ) ) ;
#4209=CARTESIAN_POINT ( 'NONE',  ( 0.000000000000000000, 104.1554980190242361, 22.75000000000000000 ) ) ;
#4212=DIRECTION ( 'NONE',  ( 0.000000000000000000, -1.000000000000000000, 0.000000000000000000 ) ) ;
#4215=CIRCLE ( 'NONE', #7765, 2.000000000000001776 ) ;
#4219=EDGE_LOOP ( 'NONE', ( #12685, #13327, #1233, #5622 ) ) ;
#4223=AXIS2_PLACEMENT_3D ( 'NONE', #4380, #3274, #174 ) ;
#4228=ORIENTED_EDGE ( 'NONE', *, *, #2124, .T. ) ;
#4229=CYLINDRICAL_SURFACE ( 'NONE', #4493, 10.00000000000000178 ) ;
#4230=CARTESIAN_POINT ( 'NONE',  ( 112.1804561881462945, 113.0390816101113387, 0.7500000000000006661 ) ) ;
#4233=CARTESIAN_POINT ( 'NONE',  ( 50.63563590245420443, 89.90549801902423610, 23.00000000000000000 ) ) ;
#4234=AXIS2_PLACEMENT_3D ( 'NONE', #10740, #8704, #8628 ) ;
#4235=ORIENTED_EDGE ( 'NONE', *, *, #9214, .T. ) ;
#4240=EDGE_CURVE ( 'NONE', #5520, #12460, #8390, .T. ) ;
#4241=( NAMED_UNIT ( * ) SI_UNIT ( $, .STERADIAN. ) SOLID_ANGLE_UNIT ( ) );
#4246=DIRECTION ( 'NONE',  ( -0.000000000000000000, -0.000000000000000000, -1.000000000000000000 ) ) ;
#4253=AXIS2_PLACEMENT_3D ( 'NONE', #3605, #4637, #8900 ) ;
#4254=EDGE_CURVE ( 'NONE', #3193, #1212, #4004, .T. ) ;
#4261=AXIS2_PLACEMENT_3D ( 'NONE', #7045, #2761, #1680 ) ;
#4271=ADVANCED_FACE ( 'NONE', ( #10488 ), #917, .F. ) ;
#4272=AXIS2_PLACEMENT_3D ( 'NONE', #9745, #9829, #11200 ) ;
#4275=ORIENTED_EDGE ( 'NONE', *, *, #3146, .F. ) ;
#4297=ORIENTED_EDGE ( 'NONE', *, *, #770, .T. ) ;
#4303=CARTESIAN_POINT ( 'NONE',  ( 84.99521369064696330, 82.14063840035363739, 10.00000000000000000 ) ) ;
#4306=PRODUCT_CONTEXT ( 'NONE', #12857, 'mechanical' ) ;
#4309=AXIS2_PLACEMENT_3D ( 'NONE', #8132, #3887, #13504 ) ;
#4312=DIRECTION ( 'NONE',  ( -0.7071067811865525687, -0.7071067811865425767, 0.000000000000000000 ) ) ;
#4313=CYLINDRICAL_SURFACE ( 'NONE', #7814, 0.7500000000000006661 ) ;
#4314=CARTESIAN_POINT ( 'NONE',  ( 72.18094369249178044, 97.20665973629650125, 10.00000000000000000 ) ) ;
#4320=CARTESIAN_POINT ( 'NONE',  ( 140.6356359024541689, 85.03908161011133870, 19.25000000000000000 ) ) ;
#4322=CYLINDRICAL_SURFACE ( 'NONE', #11375, 0.7499999999999973355 ) ;
#4326=CIRCLE ( 'NONE', #3662, 23.29163056034261459 ) ;
#4327=DIRECTION ( 'NONE',  ( -1.000000000000000000, 0.000000000000000000, 0.000000000000000000 ) ) ;
#4329=VERTEX_POINT ( 'NONE', #11805 ) ;
#4335=DIRECTION ( 'NONE',  ( 0.000000000000000000, 0.000000000000000000, -1.000000000000000000 ) ) ;
#4338=ADVANCED_FACE ( 'NONE', ( #9508 ), #3294, .T. ) ;
#4340=ADVANCED_FACE ( 'NONE', ( #10624 ), #8737, .T. ) ;
#4341=AXIS2_PLACEMENT_3D ( 'NONE', #3930, #13090, #5874 ) ;
#4342=LINE ( 'NONE', #7509, #1456 ) ;
#4347=DIRECTION ( 'NONE',  ( -0.7091883091770476710, -0.7050191076322684935, 0.000000000000000000 ) ) ;
#4354=ORIENTED_EDGE ( 'NONE', *, *, #712, .F. ) ;
#4355=ORIENTED_EDGE ( 'NONE', *, *, #9403, .T. ) ;
#4363=CARTESIAN_POINT ( 'NONE',  ( 42.63563590245419732, 85.78908161011133870, 0.7500000000000006661 ) ) ;
#4364=VERTEX_POINT ( 'NONE', #9576 ) ;
#4368=DIRECTION ( 'NONE',  ( -0.000000000000000000, -0.000000000000000000, -1.000000000000000000 ) ) ;
#4371=ORIENTED_EDGE ( 'NONE', *, *, #12206, .F. ) ;
#4373=EDGE_CURVE ( 'NONE', #3613, #7715, #5, .T. ) ;
#4380=CARTESIAN_POINT ( 'NONE',  ( 81.82136590429890077, 114.1051029460540605, 20.00000000000000000 ) ) ;
#4382=DIRECTION ( 'NONE',  ( 0.7071067811865451302, -0.7071067811865500152, 0.000000000000000000 ) ) ;
#4387=ORIENTED_EDGE ( 'NONE', *, *, #2385, .T. ) ;
#4388=VERTEX_POINT ( 'NONE', #7391 ) ;
#4389=DIRECTION ( 'NONE',  ( 1.000000000000000000, 0.000000000000000000, 0.000000000000000000 ) ) ;
#4394=CYLINDRICAL_SURFACE ( 'NONE', #12009, 0.7500000000000006661 ) ;
#4413=EDGE_CURVE ( 'NONE', #8730, #4170, #9072, .T. ) ;
#4414=AXIS2_PLACEMENT_3D ( 'NONE', #6452, #29, #13773 ) ;
#4415=VECTOR ( 'NONE', #5389, 1000.000000000000000 ) ;
#4419=CARTESIAN_POINT ( 'NONE',  ( 142.6356359024541973, 111.0390816101113103, 19.68933982822018081 ) ) ;
#4422=( BOUNDED_CURVE ( )  B_SPLINE_CURVE ( 3, ( #12671, #2076, #3255, #2284 ),
 .UNSPECIFIED., .F., .T. ) 
 B_SPLINE_CURVE_WITH_KNOTS ( ( 4, 4 ),
 ( 1.570796326794896558, 3.141592653589793116 ),
 .UNSPECIFIED. ) 
 CURVE ( )  GEOMETRIC_REPRESENTATION_ITEM ( )  RATIONAL_B_SPLINE_CURVE ( ( 1.000000000000000000, 0.8047378541243649375, 0.8047378541243649375, 1.000000000000000000 ) ) 
 REPRESENTATION_ITEM ( '' )  );
#4433=ADVANCED_FACE ( 'NONE', ( #1401 ), #5581, .T. ) ;
#4439=VECTOR ( 'NONE', #10838, 1000.000000000000000 ) ;
#4447=EDGE_CURVE ( 'NONE', #2636, #7944, #2610, .T. ) ;
#4448=CYLINDRICAL_SURFACE ( 'NONE', #11634, 6.000000000000005329 ) ;
#4452=CARTESIAN_POINT ( 'NONE',  ( 140.3249757306743675, 85.78908161011133870, 20.00000000000000000 ) ) ;
#4458=VERTEX_POINT ( 'NONE', #2681 ) ;
#4459=CARTESIAN_POINT ( 'NONE',  ( 50.63563590245420443, 108.9054980190242503, 23.00000000000000000 ) ) ;
#4462=CARTESIAN_POINT ( 'NONE',  ( 50.63563590245420443, 103.9054980190242361, 22.75000000000000000 ) ) ;
#4463=PLANE ( 'NONE',  #5727 ) ;
#4464=CARTESIAN_POINT ( 'NONE',  ( 116.7775623211734342, 85.78908161011133870, 19.25000000000000000 ) ) ;
#4471=VECTOR ( 'NONE', #188, 1000.000000000000000 ) ;
#4472=AXIS2_PLACEMENT_3D ( 'NONE', #9494, #12258, #6283 ) ;
#4473=AXIS2_PLACEMENT_3D ( 'NONE', #9249, #9096, #10300 ) ;
#4474=ORIENTED_EDGE ( 'NONE', *, *, #7926, .F. ) ;
#4479=EDGE_LOOP ( 'NONE', ( #12259, #5174, #9103, #7571 ) ) ;
#4481=AXIS2_PLACEMENT_3D ( 'NONE', #5177, #13692, #7323 ) ;
#4482=AXIS2_PLACEMENT_3D ( 'NONE', #4599, #12145, #540 ) ;
#4490=VERTEX_POINT ( 'NONE', #7812 ) ;
#4493=AXIS2_PLACEMENT_3D ( 'NONE', #1271, #12940, #7464 ) ;
#4495=VERTEX_POINT ( 'NONE', #6776 ) ;
#4500=ORIENTED_EDGE ( 'NONE', *, *, #75, .T. ) ;
#4510=ADVANCED_FACE ( 'NONE', ( #4552 ), #13063, .T. ) ;
#4521=EDGE_LOOP ( 'NONE', ( #12800, #9394, #11528, #2099 ) ) ;
#4528=EDGE_CURVE ( 'NONE', #1552, #1301, #6944, .T. ) ;
#4529=ORIENTED_EDGE ( 'NONE', *, *, #8063, .F. ) ;
#4534=DIRECTION ( 'NONE',  ( -1.000000000000000000, 0.000000000000000000, -0.000000000000000000 ) ) ;
#4543=DIRECTION ( 'NONE',  ( 0.000000000000000000, -0.000000000000000000, 1.000000000000000000 ) ) ;
#4545=TOROIDAL_SURFACE ( 'NONE', #9906, 10.75000000000000000, 0.7500000000000000000 ) ;
#4552=FACE_OUTER_BOUND ( 'NONE', #9834, .T. ) ;
#4571=EDGE_CURVE ( 'NONE', #1567, #9992, #4065, .T. ) ;
#4595=CARTESIAN_POINT ( 'NONE',  ( 79.82136590429890077, 114.1051029460540605, 20.00000000000000000 ) ) ;
#4599=CARTESIAN_POINT ( 'NONE',  ( 111.0903281124166710, 100.8715034839261762, 20.00000000000000000 ) ) ;
#4606=CARTESIAN_POINT ( 'NONE',  ( 43.38563590245419732, 87.34974178189119698, 0.000000000000000000 ) ) ;
#4612=VERTEX_POINT ( 'NONE', #3160 ) ;
#4618=DIRECTION ( 'NONE',  ( -0.000000000000000000, -0.000000000000000000, -1.000000000000000000 ) ) ;
#4619=DIRECTION ( 'NONE',  ( 0.000000000000000000, 0.000000000000000000, 1.000000000000000000 ) ) ;
#4637=DIRECTION ( 'NONE',  ( 0.000000000000000000, 0.000000000000000000, 1.000000000000000000 ) ) ;
#4640=( GEOMETRIC_REPRESENTATION_CONTEXT ( 3 ) GLOBAL_UNCERTAINTY_ASSIGNED_CONTEXT ( ( #6697 ) ) GLOBAL_UNIT_ASSIGNED_CONTEXT ( ( #9613, #13787, #4241 ) ) REPRESENTATION_CONTEXT ( 'NONE', 'WORKASPACE' ) );
#4645=EDGE_LOOP ( 'NONE', ( #6622, #5722, #8597, #1606 ) ) ;
#4647=ORIENTED_EDGE ( 'NONE', *, *, #3225, .T. ) ;
#4667=EDGE_CURVE ( 'NONE', #4388, #10924, #6409, .T. ) ;
#4668=LINE ( 'NONE', #13040, #1464 ) ;
#4680=AXIS2_PLACEMENT_3D ( 'NONE', #6338, #11851, #259 ) ;
#4682=CARTESIAN_POINT ( 'NONE',  ( 134.6356359024541973, 89.90549801902423610, 23.00000000000000000 ) ) ;
#4683=DIRECTION ( 'NONE',  ( -0.000000000000000000, 1.000000000000000000, -0.000000000000000000 ) ) ;
#4688=EDGE_LOOP ( 'NONE', ( #12739, #7200, #3891, #1472 ) ) ;
#4696=EDGE_CURVE ( 'NONE', #1212, #13218, #1833, .T. ) ;
#4699=VECTOR ( 'NONE', #6632, 1000.000000000000000 ) ;
#4701=ADVANCED_FACE ( 'NONE', ( #7935 ), #3692, .T. ) ;
#4704=ORIENTED_EDGE ( 'NONE', *, *, #5555, .T. ) ;
#4707=ORIENTED_EDGE ( 'NONE', *, *, #299, .F. ) ;
#4708=VECTOR ( 'NONE', #5919, 1000.000000000000000 ) ;
#4710=AXIS2_PLACEMENT_3D ( 'NONE', #3430, #3105, #8858 ) ;
#4724=VERTEX_POINT ( 'NONE', #5842 ) ;
#4730=CIRCLE ( 'NONE', #931, 2.000000000000001776 ) ;
#4749=CARTESIAN_POINT ( 'NONE',  ( 42.94629607423402007, 87.16776126655173584, 3.521624574640407997E-16 ) ) ;
#4750=CARTESIAN_POINT ( 'NONE',  ( 44.63563590245423285, 113.0390816101113387, 0.3106601717798216367 ) ) ;
#4765=AXIS2_PLACEMENT_3D ( 'NONE', #3524, #8185, #12178 ) ;
#4768=EDGE_CURVE ( 'NONE', #182, #2876, #6690, .T. ) ;
#4770=ORIENTED_EDGE ( 'NONE', *, *, #4165, .T. ) ;
#4790=LINE ( 'NONE', #3680, #198 ) ;
#4791=DIRECTION ( 'NONE',  ( 1.000000000000000000, 0.000000000000000000, 0.000000000000000000 ) ) ;
#4804=LINE ( 'NONE', #1726, #9566 ) ;
#4805=CARTESIAN_POINT ( 'NONE',  ( 0.000000000000000000, 0.000000000000000000, 23.00000000000000000 ) ) ;
#4812=CARTESIAN_POINT ( 'NONE',  ( 42.94629607423402007, 110.9104019536709842, 4.059660689008197386E-16 ) ) ;
#4820=CARTESIAN_POINT ( 'NONE',  ( 140.3856359024541973, 94.65549801902425031, 23.00000000000000000 ) ) ;
#4825=VERTEX_POINT ( 'NONE', #2594 ) ;
#4833=CARTESIAN_POINT ( 'NONE',  ( 50.63563590245420443, 89.90549801902423610, 20.00000000000000000 ) ) ;
#4840=DIRECTION ( 'NONE',  ( -0.7071067811865524577, -0.7071067811865425767, 0.000000000000000000 ) ) ;
#4855=AXIS2_PLACEMENT_3D ( 'NONE', #4303, #3057, #9674 ) ;
#4858=PLANE ( 'NONE',  #11636 ) ;
#4864=AXIS2_PLACEMENT_3D ( 'NONE', #13681, #8169, #2888 ) ;
#4868=CARTESIAN_POINT ( 'NONE',  ( 92.63563590245421153, 99.03908161011133870, 0.000000000000000000 ) ) ;
#4870=ORIENTED_EDGE ( 'NONE', *, *, #9029, .F. ) ;
#4871=DIRECTION ( 'NONE',  ( 1.000000000000000000, 0.000000000000000000, 0.000000000000000000 ) ) ;
#4876=CARTESIAN_POINT ( 'NONE',  ( 92.63563590245421153, 85.78908161011133870, 0.000000000000000000 ) ) ;
#4879=EDGE_CURVE ( 'NONE', #2779, #3533, #960, .T. ) ;
#4880=FACE_OUTER_BOUND ( 'NONE', #3039, .T. ) ;
#4884=VECTOR ( 'NONE', #1237, 1000.000000000000000 ) ;
#4888=CARTESIAN_POINT ( 'NONE',  ( 44.88563590245420443, 90.15549801902423610, 23.00000000000000000 ) ) ;
#4890=AXIS2_PLACEMENT_3D ( 'NONE', #7519, #6430, #10910 ) ;
#4897=DIRECTION ( 'NONE',  ( -1.000000000000000000, 0.000000000000000000, 0.000000000000000000 ) ) ;
#4904=VERTEX_POINT ( 'NONE', #13520 ) ;
#4906=ORIENTED_EDGE ( 'NONE', *, *, #4090, .T. ) ;
#4912=CARTESIAN_POINT ( 'NONE',  ( 44.88563590245420443, 108.9054980190242503, 22.75000000000000000 ) ) ;
#4917=FACE_OUTER_BOUND ( 'NONE', #13215, .T. ) ;
#4924=FACE_OUTER_BOUND ( 'NONE', #9763, .T. ) ;
#4927=DIRECTION ( 'NONE',  ( -0.7050191076322684935, 0.7091883091770476710, 0.000000000000000000 ) ) ;
#4931=VECTOR ( 'NONE', #9276, 1000.000000000000000 ) ;
#4933=EDGE_CURVE ( 'NONE', #1569, #7689, #10316, .T. ) ;
#4941=CARTESIAN_POINT ( 'NONE',  ( 50.63563590245420443, 94.90549801902425031, 23.00000000000000000 ) ) ;
#4954=ORIENTED_EDGE ( 'NONE', *, *, #11649, .T. ) ;
#4963=LINE ( 'NONE', #4195, #10896 ) ;
#4965=CYLINDRICAL_SURFACE ( 'NONE', #8141, 9.999999999999994671 ) ;
#4968=EDGE_CURVE ( 'NONE', #4364, #4458, #13388, .T. ) ;
#4974=DIRECTION ( 'NONE',  ( -0.7050191076322684935, 0.7091883091770476710, 0.000000000000000000 ) ) ;
#4981=CARTESIAN_POINT ( 'NONE',  ( 101.4499059006094512, 83.97306027416853169, 20.00000000000000000 ) ) ;
#4982=VERTEX_POINT ( 'NONE', #7090 ) ;
#4989=EDGE_CURVE ( 'NONE', #12460, #4495, #3072, .T. ) ;
#4994=DIRECTION ( 'NONE',  ( 1.000000000000000000, 0.000000000000000000, 0.000000000000000000 ) ) ;
#5009=LINE ( 'NONE', #5074, #4931 ) ;
#5010=CARTESIAN_POINT ( 'NONE',  ( 44.63563590245422574, 113.0390816101113387, 0.7500000000000006661 ) ) ;
#5016=ORIENTED_EDGE ( 'NONE', *, *, #332, .T. ) ;
#5023=PLANE ( 'NONE',  #8650 ) ;
#5032=CARTESIAN_POINT ( 'NONE',  ( 140.3856359024541973, 90.15549801902423610, 23.00000000000000000 ) ) ;
#5043=ORIENTED_EDGE ( 'NONE', *, *, #7984, .T. ) ;
#5045=ORIENTED_EDGE ( 'NONE', *, *, #5268, .T. ) ;
#5050=DIRECTION ( 'NONE',  ( 1.000000000000000000, 0.000000000000000000, -0.000000000000000000 ) ) ;
#5053=DIRECTION ( 'NONE',  ( -0.000000000000000000, -0.000000000000000000, -1.000000000000000000 ) ) ;
#5055=DIRECTION ( 'NONE',  ( -0.7091883091770476710, -0.7050191076322684935, 0.000000000000000000 ) ) ;
#5057=ORIENTED_EDGE ( 'NONE', *, *, #3739, .F. ) ;
#5064=ORIENTED_EDGE ( 'NONE', *, *, #5921, .T. ) ;
#5068=LINE ( 'NONE', #4941, #9076 ) ;
#5074=CARTESIAN_POINT ( 'NONE',  ( 140.3856359024541973, 94.90549801902425031, 23.00000000000000000 ) ) ;
#5075=PLANE ( 'NONE',  #5873 ) ;
#5083=LINE ( 'NONE', #9431, #9042 ) ;
#5100=EDGE_LOOP ( 'NONE', ( #8306, #10393 ) ) ;
#5101=VECTOR ( 'NONE', #13428, 1000.000000000000000 ) ;
#5117=ADVANCED_FACE ( 'NONE', ( #12760 ), #13725, .T. ) ;
#5128=CARTESIAN_POINT ( 'NONE',  ( 100.2760581142613603, 115.9375248198690826, 20.00000000000000000 ) ) ;
#5129=DIRECTION ( 'NONE',  ( 1.000000000000000000, 0.000000000000000000, -0.000000000000000000 ) ) ;
#5130=VERTEX_POINT ( 'NONE', #7560 ) ;
#5131=ORIENTED_EDGE ( 'NONE', *, *, #4571, .F. ) ;
#5134=TOROIDAL_SURFACE ( 'NONE', #1794, 23.29163056034262169, 0.7500000000000000000 ) ;
#5138=DIRECTION ( 'NONE',  ( 1.000000000000000000, 0.000000000000000000, 0.000000000000000000 ) ) ;
#5140=CARTESIAN_POINT ( 'NONE',  ( 140.3856359024541973, 108.9054980190242503, 23.00000000000000000 ) ) ;
#5141=AXIS2_PLACEMENT_3D ( 'NONE', #9913, #1509, #13247 ) ;
#5146=VECTOR ( 'NONE', #8792, 1000.000000000000000 ) ;
#5151=DIRECTION ( 'NONE',  ( 0.000000000000000000, -0.000000000000000000, -1.000000000000000000 ) ) ;
#5152=CARTESIAN_POINT ( 'NONE',  ( 44.88563590245420443, 104.1554980190242361, 23.00000000000000000 ) ) ;
#5157=VECTOR ( 'NONE', #6450, 999.9999999999998863 ) ;
#5159=ORIENTED_EDGE ( 'NONE', *, *, #88, .F. ) ;
#5164=EDGE_CURVE ( 'NONE', #12860, #13545, #505, .T. ) ;
#5166=EDGE_CURVE ( 'NONE', #1998, #1301, #6597, .T. ) ;
#5170=ORIENTED_EDGE ( 'NONE', *, *, #9124, .T. ) ;
#5173=VERTEX_POINT ( 'NONE', #12128 ) ;
#5174=ORIENTED_EDGE ( 'NONE', *, *, #7725, .T. ) ;
#5176=CARTESIAN_POINT ( 'NONE',  ( 44.63563590245420443, 108.9054980190242503, 20.00000000000000000 ) ) ;
#5177=CARTESIAN_POINT ( 'NONE',  ( 42.63563590245419732, 111.0390816101113387, 20.00000000000000000 ) ) ;
#5193=CARTESIAN_POINT ( 'NONE',  ( 42.63563590245419732, 87.03908161011138134, 19.68933982822018081 ) ) ;
#5199=DIRECTION ( 'NONE',  ( 0.000000000000000000, 0.000000000000000000, 1.000000000000000000 ) ) ;
#5203=EDGE_LOOP ( 'NONE', ( #11665, #6449, #13404, #6649 ) ) ;
#5205=CYLINDRICAL_SURFACE ( 'NONE', #792, 2.000000000000001776 ) ;
#5209=CARTESIAN_POINT ( 'NONE',  ( 140.6356359024541973, 113.0390816101113387, 19.25000000000000000 ) ) ;
#5215=DIRECTION ( 'NONE',  ( 1.000000000000000000, 1.290957005378089519E-15, 0.000000000000000000 ) ) ;
#5216=CARTESIAN_POINT ( 'NONE',  ( 42.63563590245419732, 111.0390816101113387, 19.25000000000000000 ) ) ;
#5218=ORIENTED_EDGE ( 'NONE', *, *, #577, .F. ) ;
#5220=CARTESIAN_POINT ( 'NONE',  ( 140.6356359024541973, 94.90549801902425031, 22.75000000000000000 ) ) ;
#5221=EDGE_LOOP ( 'NONE', ( #11359, #5159, #2907, #7001 ) ) ;
#5228=( BOUNDED_CURVE ( )  B_SPLINE_CURVE ( 3, ( #9860, #6827, #4749, #4606 ),
 .UNSPECIFIED., .F., .F. ) 
 B_SPLINE_CURVE_WITH_KNOTS ( ( 4, 4 ),
 ( 0.000000000000000000, 1.570796326794896558 ),
 .UNSPECIFIED. ) 
 CURVE ( )  GEOMETRIC_REPRESENTATION_ITEM ( )  RATIONAL_B_SPLINE_CURVE ( ( 1.000000000000000000, 0.8047378541243649375, 0.8047378541243649375, 1.000000000000000000 ) ) 
 REPRESENTATION_ITEM ( '' )  );
#5234=EDGE_LOOP ( 'NONE', ( #8977, #11823, #8325, #9265 ) ) ;
#5236=LINE ( 'NONE', #13298, #9060 ) ;
#5243=CIRCLE ( 'NONE', #6586, 9.999999999999994671 ) ;
#5245=EDGE_CURVE ( 'NONE', #11588, #11467, #1169, .T. ) ;
#5249=DIRECTION ( 'NONE',  ( 1.000000000000000000, 0.000000000000000000, 0.000000000000000000 ) ) ;
#5258=DIRECTION ( 'NONE',  ( 0.000000000000000000, -0.000000000000000000, -1.000000000000000000 ) ) ;
#5268=EDGE_CURVE ( 'NONE', #4170, #6531, #13370, .T. ) ;
#5285=ORIENTED_EDGE ( 'NONE', *, *, #9968, .F. ) ;
#5291=DIRECTION ( 'NONE',  ( 0.7071067811865451302, -0.7071067811865500152, -0.000000000000000000 ) ) ;
#5292=AXIS2_PLACEMENT_3D ( 'NONE', #10309, #5053, #10370 ) ;
#5300=VECTOR ( 'NONE', #7585, 1000.000000000000114 ) ;
#5307=CARTESIAN_POINT ( 'NONE',  ( 75.58559257550551536, 82.08927268643400055, 0.7500000000000006661 ) ) ;
#5310=( GEOMETRIC_REPRESENTATION_CONTEXT ( 3 ) GLOBAL_UNCERTAINTY_ASSIGNED_CONTEXT ( ( #12986 ) ) GLOBAL_UNIT_ASSIGNED_CONTEXT ( ( #2098, #9840, #5477 ) ) REPRESENTATION_CONTEXT ( 'NONE', 'WORKASPACE' ) );
#5316=ORIENTED_EDGE ( 'NONE', *, *, #13055, .T. ) ;
#5320=LINE ( 'NONE', #10714, #1979 ) ;
#5329=EDGE_LOOP ( 'NONE', ( #7829, #836, #7966, #761 ) ) ;
#5334=ORIENTED_EDGE ( 'NONE', *, *, #1432, .F. ) ;
#5350=EDGE_CURVE ( 'NONE', #9587, #10693, #656, .T. ) ;
#5361=ADVANCED_FACE ( 'NONE', ( #4924 ), #5951, .T. ) ;
#5362=DIRECTION ( 'NONE',  ( 0.000000000000000000, 0.000000000000000000, 1.000000000000000000 ) ) ;
#5363=AXIS2_PLACEMENT_3D ( 'NONE', #10729, #1150, #7281 ) ;
#5369=ORIENTED_EDGE ( 'NONE', *, *, #11211, .F. ) ;
#5383=ORIENTED_EDGE ( 'NONE', *, *, #88, .T. ) ;
#5388=ORIENTED_EDGE ( 'NONE', *, *, #5766, .F. ) ;
#5389=DIRECTION ( 'NONE',  ( 1.000000000000000000, -0.000000000000000000, -0.000000000000000000 ) ) ;
#5390=CYLINDRICAL_SURFACE ( 'NONE', #11780, 0.7500000000000000000 ) ;
#5391=EDGE_LOOP ( 'NONE', ( #13555, #9828, #5064, #1886 ) ) ;
#5394=DIRECTION ( 'NONE',  ( 0.000000000000000000, -1.000000000000000000, 0.000000000000000000 ) ) ;
#5398=ADVANCED_BREP_SHAPE_REPRESENTATION ( '', ( #9635, #6434 ), #5310 ) ;
#5404=EDGE_CURVE ( 'NONE', #11879, #1026, #6451, .T. ) ;
#5409=FACE_OUTER_BOUND ( 'NONE', #10244, .T. ) ;
#5420=AXIS2_PLACEMENT_3D ( 'NONE', #4682, #7941, #4543 ) ;
#5423=ORIENTED_EDGE ( 'NONE', *, *, #13232, .T. ) ;
#5428=DIRECTION ( 'NONE',  ( 1.000000000000000000, 0.000000000000000000, -0.000000000000000000 ) ) ;
#5429=DIRECTION ( 'NONE',  ( -0.000000000000000000, -0.000000000000000000, 1.000000000000000000 ) ) ;
#5433=ORIENTED_EDGE ( 'NONE', *, *, #9877, .F. ) ;
#5434=ADVANCED_FACE ( 'NONE', ( #2210 ), #10514, .T. ) ;
#5437=FACE_OUTER_BOUND ( 'NONE', #6074, .T. ) ;
#5441=CARTESIAN_POINT ( 'NONE',  ( 140.3856359024541973, 0.000000000000000000, 22.75000000000000000 ) ) ;
#5445=VECTOR ( 'NONE', #1614, 1000.000000000000000 ) ;
#5446=LINE ( 'NONE', #2416, #8810 ) ;
#5457=CYLINDRICAL_SURFACE ( 'NONE', #4414, 0.7500000000000000000 ) ;
#5465=CIRCLE ( 'NONE', #2840, 10.74999999999999645 ) ;
#5466=DIRECTION ( 'NONE',  ( -0.7050191076322684935, -0.7091883091770476710, -0.000000000000000000 ) ) ;
#5469=DIRECTION ( 'NONE',  ( 0.000000000000000000, 0.000000000000000000, 1.000000000000000000 ) ) ;
#5477=( NAMED_UNIT ( * ) SI_UNIT ( $, .STERADIAN. ) SOLID_ANGLE_UNIT ( ) );
#5480=ORIENTED_EDGE ( 'NONE', *, *, #5812, .T. ) ;
#5484=LINE ( 'NONE', #10816, #7137 ) ;
#5490=CARTESIAN_POINT ( 'NONE',  ( 43.16596598834411225, 87.56941169600128205, 0.000000000000000000 ) ) ;
#5493=CARTESIAN_POINT ( 'NONE',  ( 103.4499059006094512, 83.97306027416853169, 10.00000000000000000 ) ) ;
#5507=LINE ( 'NONE', #12918, #11563 ) ;
#5508=CIRCLE ( 'NONE', #13323, 2.000000000000001776 ) ;
#5513=VECTOR ( 'NONE', #6614, 1000.000000000000000 ) ;
#5514=ORIENTED_EDGE ( 'NONE', *, *, #10939, .T. ) ;
#5517=VERTEX_POINT ( 'NONE', #12941 ) ;
#5520=VERTEX_POINT ( 'NONE', #3603 ) ;
#5521=ORIENTED_EDGE ( 'NONE', *, *, #7031, .F. ) ;
#5524=ORIENTED_EDGE ( 'NONE', *, *, #13395, .F. ) ;
#5530=AXIS2_PLACEMENT_3D ( 'NONE', #7870, #8791, #6962 ) ;
#5531=CARTESIAN_POINT ( 'NONE',  ( 92.63563590245421153, 99.03908161011133870, 0.000000000000000000 ) ) ;
#5533=VECTOR ( 'NONE', #3370, 1000.000000000000000 ) ;
#5538=AXIS2_PLACEMENT_3D ( 'NONE', #1893, #827, #6131 ) ;
#5539=CIRCLE ( 'NONE', #10684, 9.999999999999994671 ) ;
#5541=DIRECTION ( 'NONE',  ( 0.000000000000000000, 1.000000000000000000, 0.000000000000000000 ) ) ;
#5543=CARTESIAN_POINT ( 'NONE',  ( 92.63563590245421153, 99.03908161011133870, 19.25000000000000000 ) ) ;
#5554=AXIS2_PLACEMENT_3D ( 'NONE', #11844, #12684, #2365 ) ;
#5555=EDGE_CURVE ( 'NONE', #3595, #10924, #2565, .T. ) ;
#5556=ORIENTED_EDGE ( 'NONE', *, *, #13260, .F. ) ;
#5558=ADVANCED_FACE ( 'NONE', ( #1350 ), #2101, .T. ) ;
#5571=CARTESIAN_POINT ( 'NONE',  ( 84.99521369064696330, 82.14063840035363739, 10.00000000000000000 ) ) ;
#5574=VECTOR ( 'NONE', #5429, 1000.000000000000000 ) ;
#5581=CYLINDRICAL_SURFACE ( 'NONE', #11859, 0.7500000000000006661 ) ;
#5583=LINE ( 'NONE', #3369, #4439 ) ;
#5587=CYLINDRICAL_SURFACE ( 'NONE', #8259, 0.7500000000000006661 ) ;
#5592=DIRECTION ( 'NONE',  ( -0.000000000000000000, -0.000000000000000000, -1.000000000000000000 ) ) ;
#5607=EDGE_CURVE ( 'NONE', #3428, #6986, #305, .T. ) ;
#5609=AXIS2_PLACEMENT_3D ( 'NONE', #4193, #8439, #7305 ) ;
#5612=AXIS2_PLACEMENT_3D ( 'NONE', #9154, #13477, #1609 ) ;
#5616=CARTESIAN_POINT ( 'NONE',  ( 86.99521369064697751, 82.14063840035363739, 10.00000000000000000 ) ) ;
#5619=ADVANCED_FACE ( 'NONE', ( #5810 ), #4545, .T. ) ;
#5622=ORIENTED_EDGE ( 'NONE', *, *, #5607, .T. ) ;
#5623=CARTESIAN_POINT ( 'NONE',  ( 142.6356359024541973, 87.03908161011133870, 20.00000000000000000 ) ) ;
#5624=CARTESIAN_POINT ( 'NONE',  ( 68.49370948373500312, 85.78908161011133870, 0.000000000000000000 ) ) ;
#5628=ORIENTED_EDGE ( 'NONE', *, *, #2385, .F. ) ;
#5632=CARTESIAN_POINT ( 'NONE',  ( 76.18094369249178044, 97.20665973629650125, 10.00000000000000000 ) ) ;
#5636=FACE_OUTER_BOUND ( 'NONE', #12012, .T. ) ;
#5641=CARTESIAN_POINT ( 'NONE',  ( 141.8856359024541973, 110.7284214383315089, 0.000000000000000000 ) ) ;
#5650=DIRECTION ( 'NONE',  ( 0.000000000000000000, 0.000000000000000000, -1.000000000000000000 ) ) ;
#5651=LINE ( 'NONE', #6976, #9122 ) ;
#5652=DIRECTION ( 'NONE',  ( 0.000000000000000000, 0.000000000000000000, -1.000000000000000000 ) ) ;
#5658=ORIENTED_EDGE ( 'NONE', *, *, #12696, .T. ) ;
#5661=ORIENTED_EDGE ( 'NONE', *, *, #13260, .T. ) ;
#5664=LINE ( 'NONE', #3521, #9778 ) ;
#5668=CARTESIAN_POINT ( 'NONE',  ( 116.7775623211734342, 112.2890816101113387, 20.00000000000000000 ) ) ;
#5672=( BOUNDED_CURVE ( )  B_SPLINE_CURVE ( 3, ( #1894, #829, #1966, #3920 ),
 .UNSPECIFIED., .F., .F. ) 
 B_SPLINE_CURVE_WITH_KNOTS ( ( 4, 4 ),
 ( 1.570796326794896558, 3.141592653589793116 ),
 .UNSPECIFIED. ) 
 CURVE ( )  GEOMETRIC_REPRESENTATION_ITEM ( )  RATIONAL_B_SPLINE_CURVE ( ( 1.000000000000000000, 0.8047378541243649375, 0.8047378541243649375, 1.000000000000000000 ) ) 
 REPRESENTATION_ITEM ( '' )  );
#5683=DIRECTION ( 'NONE',  ( -1.000000000000000000, 0.000000000000000000, 0.000000000000000000 ) ) ;
#5691=ORIENTED_EDGE ( 'NONE', *, *, #3225, .F. ) ;
#5692=FACE_OUTER_BOUND ( 'NONE', #9770, .T. ) ;
#5712=CARTESIAN_POINT ( 'NONE',  ( 44.63563590245421864, 85.03908161011133870, 0.7500000000000006661 ) ) ;
#5722=ORIENTED_EDGE ( 'NONE', *, *, #3146, .T. ) ;
#5727=AXIS2_PLACEMENT_3D ( 'NONE', #8719, #3423, #9639 ) ;
#5745=AXIS2_PLACEMENT_3D ( 'NONE', #9669, #9808, #3253 ) ;
#5748=CARTESIAN_POINT ( 'NONE',  ( 0.000000000000000000, 0.000000000000000000, 23.00000000000000000 ) ) ;
#5749=AXIS2_PLACEMENT_3D ( 'NONE', #10785, #1200, #12742 ) ;
#5757=ORIENTED_EDGE ( 'NONE', *, *, #13395, .T. ) ;
#5766=EDGE_CURVE ( 'NONE', #4982, #12198, #9774, .T. ) ;
#5769=FACE_OUTER_BOUND ( 'NONE', #5391, .T. ) ;
#5784=ORIENTED_EDGE ( 'NONE', *, *, #4447, .F. ) ;
#5788=CYLINDRICAL_SURFACE ( 'NONE', #5612, 2.000000000000001776 ) ;
#5791=CARTESIAN_POINT ( 'NONE',  ( 86.99521369064697751, 82.14063840035363739, 20.00000000000000000 ) ) ;
#5796=VERTEX_POINT ( 'NONE', #8260 ) ;
#5810=FACE_OUTER_BOUND ( 'NONE', #12392, .T. ) ;
#5812=EDGE_CURVE ( 'NONE', #54, #5796, #11472, .T. ) ;
#5825=CARTESIAN_POINT ( 'NONE',  ( 50.38563590245420443, 104.1554980190242361, 23.00000000000000000 ) ) ;
#5842=CARTESIAN_POINT ( 'NONE',  ( 109.1537879975201406, 82.61803701715820125, 20.00000000000000000 ) ) ;
#5845=DIRECTION ( 'NONE',  ( -0.000000000000000000, 0.000000000000000000, 1.000000000000000000 ) ) ;
#5847=CARTESIAN_POINT ( 'NONE',  ( 142.6356359024541973, 111.0390816101113245, 0.7500000000000006661 ) ) ;
#5851=EDGE_LOOP ( 'NONE', ( #3737, #10185, #13643, #2747 ) ) ;
#5860=DIRECTION ( 'NONE',  ( -0.000000000000000000, -0.000000000000000000, 1.000000000000000000 ) ) ;
#5872=ADVANCED_FACE ( 'NONE', ( #10062 ), #3765, .F. ) ;
#5873=AXIS2_PLACEMENT_3D ( 'NONE', #8091, #6056, #5151 ) ;
#5874=DIRECTION ( 'NONE',  ( 1.000000000000000000, 0.000000000000000000, 0.000000000000000000 ) ) ;
#5881=CARTESIAN_POINT ( 'NONE',  ( 140.6356359024541973, 108.9054980190242503, 22.75000000000000000 ) ) ;
#5882=CARTESIAN_POINT ( 'NONE',  ( 140.5320825118609207, 104.0090514096174843, 23.00000000000000000 ) ) ;
#5891=DIRECTION ( 'NONE',  ( 0.000000000000000000, 0.000000000000000000, 1.000000000000000000 ) ) ;
#5892=CARTESIAN_POINT ( 'NONE',  ( 68.49370948373500312, 85.78908161011133870, 20.00000000000000000 ) ) ;
#5897=CARTESIAN_POINT ( 'NONE',  ( 116.7775623211734342, 112.2890816101113387, 20.00000000000000000 ) ) ;
#5900=LINE ( 'NONE', #6956, #6248 ) ;
#5902=LINE ( 'NONE', #8402, #8646 ) ;
#5908=EDGE_CURVE ( 'NONE', #13076, #4982, #2410, .T. ) ;
#5910=CARTESIAN_POINT ( 'NONE',  ( 140.6356359024541973, 108.9054980190242503, 22.89644660940672694 ) ) ;
#5913=EDGE_LOOP ( 'NONE', ( #11744, #1481, #10995, #5966 ) ) ;
#5917=DIRECTION ( 'NONE',  ( 0.7071067811865451302, -0.7071067811865500152, -0.000000000000000000 ) ) ;
#5919=DIRECTION ( 'NONE',  ( 1.000000000000000000, -0.000000000000000000, -0.000000000000000000 ) ) ;
#5920=FACE_OUTER_BOUND ( 'NONE', #3264, .T. ) ;
#5921=EDGE_CURVE ( 'NONE', #11822, #8835, #5228, .T. ) ;
#5924=CARTESIAN_POINT ( 'NONE',  ( 116.7775623211734342, 123.0390816101113245, 20.00000000000000000 ) ) ;
#5927=ORIENTED_EDGE ( 'NONE', *, *, #8313, .T. ) ;
#5932=VERTEX_POINT ( 'NONE', #1596 ) ;
#5939=DIRECTION ( 'NONE',  ( 1.000000000000000000, 0.000000000000000000, 0.000000000000000000 ) ) ;
#5942=CARTESIAN_POINT ( 'NONE',  ( 140.6356359024541973, 103.9054980190242361, 22.75000000000000000 ) ) ;
#5945=AXIS2_PLACEMENT_3D ( 'NONE', #1097, #2170, #4389 ) ;
#5951=PLANE ( 'NONE',  #9215 ) ;
#5955=CIRCLE ( 'NONE', #2199, 10.74999999999999645 ) ;
#5964=PLANE ( 'NONE',  #9952 ) ;
#5966=ORIENTED_EDGE ( 'NONE', *, *, #6193, .F. ) ;
#5969=CARTESIAN_POINT ( 'NONE',  ( 140.6356359024541689, 85.03908161011133870, 0.7500000000000006661 ) ) ;
#5972=CARTESIAN_POINT ( 'NONE',  ( 42.63563590245420443, 111.0390816101113387, 0.7500000000000000000 ) ) ;
#5986=DIRECTION ( 'NONE',  ( -0.000000000000000000, -0.000000000000000000, 1.000000000000000000 ) ) ;
#5989=AXIS2_PLACEMENT_3D ( 'NONE', #6673, #1498, #4791 ) ;
#5991=DIRECTION ( 'NONE',  ( -1.000000000000000000, 0.000000000000000000, 0.000000000000000000 ) ) ;
#5993=CARTESIAN_POINT ( 'NONE',  ( 140.6356359024541973, 94.90549801902425031, 22.75000000000000000 ) ) ;
#5998=DIRECTION ( 'NONE',  ( -0.000000000000000000, -0.000000000000000000, -1.000000000000000000 ) ) ;
#6006=EDGE_LOOP ( 'NONE', ( #2133, #5045, #13485, #6581 ) ) ;
#6010=CARTESIAN_POINT ( 'NONE',  ( 43.38563590245419732, 87.34974178189119698, 20.00000000000000000 ) ) ;
#6014=CIRCLE ( 'NONE', #13158, 2.000000000000001776 ) ;
#6019=DIRECTION ( 'NONE',  ( -0.000000000000000000, -0.000000000000000000, 1.000000000000000000 ) ) ;
#6027=EDGE_LOOP ( 'NONE', ( #6720, #1073, #4707, #8994 ) ) ;
#6030=EDGE_CURVE ( 'NONE', #721, #2952, #6657, .T. ) ;
#6034=FACE_BOUND ( 'NONE', #9286, .T. ) ;
#6042=( BOUNDED_CURVE ( )  B_SPLINE_CURVE ( 3, ( #6696, #4750, #7942, #3643 ),
 .UNSPECIFIED., .F., .F. ) 
 B_SPLINE_CURVE_WITH_KNOTS ( ( 4, 4 ),
 ( 0.000000000000000000, 1.570796326794896558 ),
 .UNSPECIFIED. ) 
 CURVE ( )  GEOMETRIC_REPRESENTATION_ITEM ( )  RATIONAL_B_SPLINE_CURVE ( ( 1.000000000000000000, 0.8047378541243649375, 0.8047378541243649375, 1.000000000000000000 ) ) 
 REPRESENTATION_ITEM ( '' )  );
#6043=CARTESIAN_POINT ( 'NONE',  ( 92.63563590245421153, 99.03908161011133870, 0.000000000000000000 ) ) ;
#6045=EDGE_LOOP ( 'NONE', ( #2200, #2132, #6609, #11276 ) ) ;
#6046=ORIENTED_EDGE ( 'NONE', *, *, #11878, .F. ) ;
#6048=DIRECTION ( 'NONE',  ( -0.000000000000000000, -0.000000000000000000, -1.000000000000000000 ) ) ;
#6056=DIRECTION ( 'NONE',  ( 0.000000000000000000, -1.000000000000000000, 0.000000000000000000 ) ) ;
#6074=EDGE_LOOP ( 'NONE', ( #12843, #9521 ) ) ;
#6077=VERTEX_POINT ( 'NONE', #1880 ) ;
#6080=VERTEX_POINT ( 'NONE', #5010 ) ;
#6084=EDGE_CURVE ( 'NONE', #1997, #54, #2487, .T. ) ;
#6088=ADVANCED_FACE ( 'NONE', ( #4880 ), #5075, .F. ) ;
#6089=EDGE_LOOP ( 'NONE', ( #844, #7489, #4036, #1503 ) ) ;
#6100=PLANE ( 'NONE',  #2033 ) ;
#6103=ORIENTED_EDGE ( 'NONE', *, *, #712, .T. ) ;
#6104=EDGE_CURVE ( 'NONE', #4904, #3980, #3443, .T. ) ;
#6105=CARTESIAN_POINT ( 'NONE',  ( 116.7775623211734342, 112.2890816101113387, 0.000000000000000000 ) ) ;
#6115=EDGE_CURVE ( 'NONE', #3543, #4612, #4326, .T. ) ;
#6116=CARTESIAN_POINT ( 'NONE',  ( 50.63563590245420443, 94.90549801902425031, 22.75000000000000000 ) ) ;
#6125=VERTEX_POINT ( 'NONE', #3015 ) ;
#6128=CARTESIAN_POINT ( 'NONE',  ( 43.38563590245419732, 87.03908161011136713, 20.00000000000000000 ) ) ;
#6131=DIRECTION ( 'NONE',  ( 1.000000000000000000, 0.000000000000000000, 0.000000000000000000 ) ) ;
#6132=EDGE_CURVE ( 'NONE', #1301, #12138, #7874, .T. ) ;
#6133=VECTOR ( 'NONE', #8712, 1000.000000000000000 ) ;
#6135=EDGE_CURVE ( 'NONE', #2697, #7324, #7786, .T. ) ;
#6136=EDGE_LOOP ( 'NONE', ( #10815, #7491, #2844, #2397 ) ) ;
#6137=AXIS2_PLACEMENT_3D ( 'NONE', #6043, #10318, #8077 ) ;
#6139=EDGE_LOOP ( 'NONE', ( #3250, #1928, #3450, #7118 ) ) ;
#6142=CARTESIAN_POINT ( 'NONE',  ( 82.99521369064696330, 82.14063840035363739, 10.00000000000000000 ) ) ;
#6143=ORIENTED_EDGE ( 'NONE', *, *, #1052, .T. ) ;
#6148=LINE ( 'NONE', #1771, #9607 ) ;
#6149=DIRECTION ( 'NONE',  ( -1.000000000000000000, -0.000000000000000000, -0.000000000000000000 ) ) ;
#6153=ORIENTED_EDGE ( 'NONE', *, *, #11445, .F. ) ;
#6161=CYLINDRICAL_SURFACE ( 'NONE', #1599, 2.000000000000001776 ) ;
#6163=CARTESIAN_POINT ( 'NONE',  ( 44.63563590245420443, 108.9054980190242503, 20.00000000000000000 ) ) ;
#6164=DIRECTION ( 'NONE',  ( 1.000000000000000000, 0.000000000000000000, 0.000000000000000000 ) ) ;
#6165=FACE_BOUND ( 'NONE', #5100, .T. ) ;
#6172=DIRECTION ( 'NONE',  ( 1.000000000000000000, 0.000000000000000000, 0.000000000000000000 ) ) ;
#6175=CARTESIAN_POINT ( 'NONE',  ( 98.27605811426136029, 115.9375248198690826, 10.00000000000000000 ) ) ;
#6178=LINE ( 'NONE', #5140, #8500 ) ;
#6180=VERTEX_POINT ( 'NONE', #9486 ) ;
#6182=CARTESIAN_POINT ( 'NONE',  ( 134.8856359024541973, 104.1554980190242361, 23.00000000000000000 ) ) ;
#6193=EDGE_CURVE ( 'NONE', #4071, #4170, #6341, .T. ) ;
#6195=ORIENTED_EDGE ( 'NONE', *, *, #7907, .F. ) ;
#6197=CIRCLE ( 'NONE', #8685, 24.04163056034261459 ) ;
#6204=ADVANCED_FACE ( 'NONE', ( #12697 ), #4322, .T. ) ;
#6206=VECTOR ( 'NONE', #7228, 1000.000000000000000 ) ;
#6218=DIRECTION ( 'NONE',  ( -0.000000000000000000, -0.000000000000000000, 1.000000000000000000 ) ) ;
#6222=ORIENTED_EDGE ( 'NONE', *, *, #12611, .T. ) ;
#6230=ORIENTED_EDGE ( 'NONE', *, *, #5164, .F. ) ;
#6235=ORIENTED_EDGE ( 'NONE', *, *, #112, .T. ) ;
#6239=EDGE_CURVE ( 'NONE', #217, #3941, #10688, .T. ) ;
#6248=VECTOR ( 'NONE', #10122, 1000.000000000000000 ) ;
#6250=VECTOR ( 'NONE', #8264, 1000.000000000000000 ) ;
#6252=ORIENTED_EDGE ( 'NONE', *, *, #13701, .T. ) ;
#6254=FACE_OUTER_BOUND ( 'NONE', #4479, .T. ) ;
#6262=VECTOR ( 'NONE', #11888, 1000.000000000000000 ) ;
#6264=DIRECTION ( 'NONE',  ( 1.000000000000000000, 0.000000000000000000, 0.000000000000000000 ) ) ;
#6268=CARTESIAN_POINT ( 'NONE',  ( 50.63563590245420443, 94.90549801902425031, 20.00000000000000000 ) ) ;
#6269=LINE ( 'NONE', #5216, #6206 ) ;
#6273=VECTOR ( 'NONE', #2188, 1000.000000000000114 ) ;
#6283=DIRECTION ( 'NONE',  ( 0.000000000000000000, 0.000000000000000000, 1.000000000000000000 ) ) ;
#6289=AXIS2_PLACEMENT_3D ( 'NONE', #5531, #3317, #12808 ) ;
#6292=ORIENTED_EDGE ( 'NONE', *, *, #10486, .T. ) ;
#6295=VERTEX_POINT ( 'NONE', #1223 ) ;
#6297=ORIENTED_EDGE ( 'NONE', *, *, #75, .F. ) ;
#6307=DIRECTION ( 'NONE',  ( -0.000000000000000000, -0.000000000000000000, -1.000000000000000000 ) ) ;
#6309=ORIENTED_EDGE ( 'NONE', *, *, #7902, .T. ) ;
#6321=DIRECTION ( 'NONE',  ( 0.000000000000000000, 0.000000000000000000, -1.000000000000000000 ) ) ;
#6324=FACE_OUTER_BOUND ( 'NONE', #6342, .T. ) ;
#6326=EDGE_CURVE ( 'NONE', #6125, #2972, #11925, .T. ) ;
#6335=SURFACE_SIDE_STYLE ('',( #9746 ) ) ;
#6338=CARTESIAN_POINT ( 'NONE',  ( 140.6356359024541973, 94.90549801902425031, 23.00000000000000000 ) ) ;
#6339=LINE ( 'NONE', #10594, #2220 ) ;
#6341=LINE ( 'NONE', #6268, #12042 ) ;
#6342=EDGE_LOOP ( 'NONE', ( #4954, #2828, #4131, #9025 ) ) ;
#6344=CARTESIAN_POINT ( 'NONE',  ( 140.5320825118609207, 94.80194462843097369, 23.00000000000000000 ) ) ;
#6346=EDGE_LOOP ( 'NONE', ( #6810, #10541, #1096, #4275 ) ) ;
#6355=EDGE_LOOP ( 'NONE', ( #365, #2603, #3661, #5691 ) ) ;
#6358=EDGE_CURVE ( 'NONE', #2858, #3543, #12923, .T. ) ;
#6361=VECTOR ( 'NONE', #7754, 1000.000000000000000 ) ;
#6366=CARTESIAN_POINT ( 'NONE',  ( 82.99521369064696330, 82.14063840035363739, 10.00000000000000000 ) ) ;
#6381=CARTESIAN_POINT ( 'NONE',  ( 50.38563590245420443, 94.90549801902425031, 22.75000000000000000 ) ) ;
#6400=DIRECTION ( 'NONE',  ( 0.7071067811865567876, 0.7071067811865382469, 0.000000000000000000 ) ) ;
#6402=CIRCLE ( 'NONE', #5945, 10.74999999999999645 ) ;
#6409=LINE ( 'NONE', #1100, #3844 ) ;
#6415=STYLED_ITEM ( 'NONE', ( #6537 ), #9635 ) ;
#6420=AXIS2_PLACEMENT_3D ( 'NONE', #13110, #3633, #10889 ) ;
#6421=VECTOR ( 'NONE', #3986, 1000.000000000000000 ) ;
#6428=ORIENTED_EDGE ( 'NONE', *, *, #12512, .T. ) ;
#6430=DIRECTION ( 'NONE',  ( 0.000000000000000000, 0.000000000000000000, 1.000000000000000000 ) ) ;
#6434=AXIS2_PLACEMENT_3D ( 'NONE', #11654, #12825, #11856 ) ;
#6449=ORIENTED_EDGE ( 'NONE', *, *, #1777, .T. ) ;
#6450=DIRECTION ( 'NONE',  ( -0.7071067811865525687, -0.7071067811865425767, 0.000000000000000000 ) ) ;
#6451=LINE ( 'NONE', #4230, #3644 ) ;
#6452=CARTESIAN_POINT ( 'NONE',  ( 43.38563590245419732, 85.03908161011133870, 0.7500000000000006661 ) ) ;
#6460=ADVANCED_FACE ( 'NONE', ( #2515, #1438, #6034, #12471, #10311, #7996, #9326, #2998, #6165, #3889, #1926, #731 ), #6100, .T. ) ;
#6463=FACE_OUTER_BOUND ( 'NONE', #8842, .T. ) ;
#6464=CYLINDRICAL_SURFACE ( 'NONE', #13763, 0.7499999999999924505 ) ;
#6466=DIRECTION ( 'NONE',  ( 0.000000000000000000, -1.000000000000000000, 0.000000000000000000 ) ) ;
#6475=EDGE_CURVE ( 'NONE', #12138, #7324, #2471, .T. ) ;
#6476=AXIS2_PLACEMENT_3D ( 'NONE', #667, #12409, #4871 ) ;
#6481=EDGE_LOOP ( 'NONE', ( #2694, #9726, #2423, #11821 ) ) ;
#6491=VECTOR ( 'NONE', #10946, 1000.000000000000000 ) ;
#6493=VECTOR ( 'NONE', #12150, 1000.000000000000000 ) ;
#6497=ORIENTED_EDGE ( 'NONE', *, *, #636, .F. ) ;
#6504=DIRECTION ( 'NONE',  ( 0.000000000000000000, 0.000000000000000000, 1.000000000000000000 ) ) ;
#6508=CARTESIAN_POINT ( 'NONE',  ( 185.2712718049083946, 90.15549801902423610, 23.00000000000000000 ) ) ;
#6510=CYLINDRICAL_SURFACE ( 'NONE', #12060, 2.000000000000001776 ) ;
#6515=ORIENTED_EDGE ( 'NONE', *, *, #11608, .F. ) ;
#6525=DIRECTION ( 'NONE',  ( 1.000000000000000000, 0.000000000000000000, 0.000000000000000000 ) ) ;
#6526=DIRECTION ( 'NONE',  ( 0.000000000000000000, -1.000000000000000000, 0.000000000000000000 ) ) ;
#6531=VERTEX_POINT ( 'NONE', #8278 ) ;
#6537=PRESENTATION_STYLE_ASSIGNMENT (( #1289 ) ) ;
#6555=CARTESIAN_POINT ( 'NONE',  ( 140.6356359024541973, 94.90549801902425031, 20.00000000000000000 ) ) ;
#6557=DIRECTION ( 'NONE',  ( 1.000000000000000000, 0.000000000000000000, 0.000000000000000000 ) ) ;
#6564=LINE ( 'NONE', #10989, #13602 ) ;
#6566=EDGE_LOOP ( 'NONE', ( #1869, #12682, #4022, #7958, #5383, #5661, #3050, #4235, #3577, #3944, #10250, #5514, #7775, #8060, #3368, #1479 ) ) ;
#6568=DIRECTION ( 'NONE',  ( -0.7071067811865500152, -0.7071067811865451302, -0.000000000000000000 ) ) ;
#6570=DIRECTION ( 'NONE',  ( -0.000000000000000000, -0.000000000000000000, 1.000000000000000000 ) ) ;
#6576=ORIENTED_EDGE ( 'NONE', *, *, #4696, .T. ) ;
#6579=DIRECTION ( 'NONE',  ( 1.000000000000000000, 0.000000000000000000, 0.000000000000000000 ) ) ;
#6581=ORIENTED_EDGE ( 'NONE', *, *, #3803, .T. ) ;
#6586=AXIS2_PLACEMENT_3D ( 'NONE', #757, #8369, #12634 ) ;
#6588=ADVANCED_FACE ( 'NONE', ( #6324 ), #5134, .T. ) ;
#6592=DIRECTION ( 'NONE',  ( 1.000000000000000000, -0.000000000000000000, -0.000000000000000000 ) ) ;
#6593=VERTEX_POINT ( 'NONE', #2215 ) ;
#6595=CYLINDRICAL_SURFACE ( 'NONE', #841, 0.2500000000000002220 ) ;
#6597=LINE ( 'NONE', #12191, #11215 ) ;
#6606=ORIENTED_EDGE ( 'NONE', *, *, #5268, .F. ) ;
#6609=ORIENTED_EDGE ( 'NONE', *, *, #11835, .T. ) ;
#6614=DIRECTION ( 'NONE',  ( 1.000000000000000000, -0.000000000000000000, -0.000000000000000000 ) ) ;
#6616=DIRECTION ( 'NONE',  ( 0.000000000000000000, 0.000000000000000000, 1.000000000000000000 ) ) ;
#6622=ORIENTED_EDGE ( 'NONE', *, *, #12098, .T. ) ;
#6624=ORIENTED_EDGE ( 'NONE', *, *, #6983, .F. ) ;
#6627=ADVANCED_FACE ( 'NONE', ( #9602 ), #10583, .F. ) ;
#6631=CARTESIAN_POINT ( 'NONE',  ( 62.16596598834396303, 68.56941169600129626, 19.25000000000000000 ) ) ;
#6632=DIRECTION ( 'NONE',  ( -0.000000000000000000, -0.000000000000000000, 1.000000000000000000 ) ) ;
#6633=DIRECTION ( 'NONE',  ( 0.000000000000000000, 0.000000000000000000, 1.000000000000000000 ) ) ;
#6639=AXIS2_PLACEMENT_3D ( 'NONE', #10432, #791, #5050 ) ;
#6649=ORIENTED_EDGE ( 'NONE', *, *, #4373, .T. ) ;
#6650=CARTESIAN_POINT ( 'NONE',  ( 81.82136590429890077, 114.1051029460540605, 10.00000000000000000 ) ) ;
#6652=VECTOR ( 'NONE', #8966, 1000.000000000000000 ) ;
#6657=( BOUNDED_CURVE ( )  B_SPLINE_CURVE ( 3, ( #8222, #2807, #5910, #12486 ),
 .UNSPECIFIED., .F., .F. ) 
 B_SPLINE_CURVE_WITH_KNOTS ( ( 4, 4 ),
 ( 1.570796326794896558, 3.141592653589793116 ),
 .UNSPECIFIED. ) 
 CURVE ( )  GEOMETRIC_REPRESENTATION_ITEM ( )  RATIONAL_B_SPLINE_CURVE ( ( 1.000000000000000000, 0.8047378541243649375, 0.8047378541243649375, 1.000000000000000000 ) ) 
 REPRESENTATION_ITEM ( '' )  );
#6660=VERTEX_POINT ( 'NONE', #3260 ) ;
#6667=CARTESIAN_POINT ( 'NONE',  ( 109.0903281124166710, 100.8715034839261762, 20.00000000000000000 ) ) ;
#6669=DIRECTION ( 'NONE',  ( 1.000000000000000000, 0.000000000000000000, 0.000000000000000000 ) ) ;
#6673=CARTESIAN_POINT ( 'NONE',  ( 116.7775623211734342, 123.0390816101113245, 19.25000000000000000 ) ) ;
#6689=AXIS2_PLACEMENT_3D ( 'NONE', #4233, #6526, #5258 ) ;
#6690=LINE ( 'NONE', #12072, #2520 ) ;
#6693=ADVANCED_FACE ( 'NONE', ( #3320 ), #10517, .T. ) ;
#6696=CARTESIAN_POINT ( 'NONE',  ( 44.63563590245422574, 113.0390816101113387, 0.7500000000000006661 ) ) ;
#6697=UNCERTAINTY_MEASURE_WITH_UNIT (LENGTH_MEASURE( 1.000000000000000082E-05 ), #9613, 'distance_accuracy_value', 'NONE');
#6706=VERTEX_POINT ( 'NONE', #948 ) ;
#6710=ORIENTED_EDGE ( 'NONE', *, *, #9531, .T. ) ;
#6720=ORIENTED_EDGE ( 'NONE', *, *, #10744, .F. ) ;
#6735=FACE_OUTER_BOUND ( 'NONE', #2895, .T. ) ;
#6743=CARTESIAN_POINT ( 'NONE',  ( 68.49370948373500312, 75.03908161011133870, 0.000000000000000000 ) ) ;
#6746=CARTESIAN_POINT ( 'NONE',  ( 68.49370948373500312, 85.78908161011133870, 0.7500000000000000000 ) ) ;
#6754=ORIENTED_EDGE ( 'NONE', *, *, #7199, .T. ) ;
#6764=CARTESIAN_POINT ( 'NONE',  ( 140.6356359024541973, 103.9054980190242361, 22.75000000000000000 ) ) ;
#6773=ORIENTED_EDGE ( 'NONE', *, *, #12076, .F. ) ;
#6774=LINE ( 'NONE', #3776, #7945 ) ;
#6776=CARTESIAN_POINT ( 'NONE',  ( 140.3856359024541973, 104.1554980190242361, 23.00000000000000000 ) ) ;
#6781=ADVANCED_FACE ( 'NONE', ( #6735 ), #11972, .F. ) ;
#6787=ORIENTED_EDGE ( 'NONE', *, *, #1883, .T. ) ;
#6792=DIRECTION ( 'NONE',  ( -0.000000000000000000, -0.000000000000000000, -1.000000000000000000 ) ) ;
#6799=ADVANCED_FACE ( 'NONE', ( #375 ), #10712, .T. ) ;
#6806=DIRECTION ( 'NONE',  ( -0.7071067811865525687, -0.7071067811865425767, 0.000000000000000000 ) ) ;
#6810=ORIENTED_EDGE ( 'NONE', *, *, #7743, .T. ) ;
#6813=AXIS2_PLACEMENT_3D ( 'NONE', #4868, #7016, #6953 ) ;
#6817=VERTEX_POINT ( 'NONE', #448 ) ;
#6821=CARTESIAN_POINT ( 'NONE',  ( 109.1537879975201406, 115.4601262030644762, 0.000000000000000000 ) ) ;
#6824=LINE ( 'NONE', #6764, #1993 ) ;
#6825=CARTESIAN_POINT ( 'NONE',  ( 68.49370948373500312, 123.0390816101113245, 0.7500000000000006661 ) ) ;
#6827=CARTESIAN_POINT ( 'NONE',  ( 42.63563590245419732, 87.03908161011138134, 0.3106601717798216367 ) ) ;
#6837=LINE ( 'NONE', #5993, #4708 ) ;
#6847=ORIENTED_EDGE ( 'NONE', *, *, #4162, .F. ) ;
#6853=LINE ( 'NONE', #8891, #12677 ) ;
#6854=ORIENTED_EDGE ( 'NONE', *, *, #7984, .F. ) ;
#6861=CIRCLE ( 'NONE', #5292, 10.74999999999999645 ) ;
#6870=CIRCLE ( 'NONE', #7988, 23.29163056034261459 ) ;
#6874=CARTESIAN_POINT ( 'NONE',  ( 134.6356359024541973, 89.90549801902423610, 20.00000000000000000 ) ) ;
#6880=VECTOR ( 'NONE', #10476, 1000.000000000000000 ) ;
#6883=ADVANCED_FACE ( 'NONE', ( #4917 ), #7198, .F. ) ;
#6886=APPLICATION_CONTEXT ( 'automotive_design' ) ;
#6887=CARTESIAN_POINT ( 'NONE',  ( 74.18094369249178044, 97.20665973629650125, 10.00000000000000000 ) ) ;
#6890=LINE ( 'NONE', #11156, #623 ) ;
#6900=EDGE_CURVE ( 'NONE', #719, #182, #4012, .T. ) ;
#6903=AXIS2_PLACEMENT_3D ( 'NONE', #11614, #6568, #1254 ) ;
#6907=CARTESIAN_POINT ( 'NONE',  ( 140.3249757306743675, 85.78908161011133870, 0.000000000000000000 ) ) ;
#6921=ORIENTED_EDGE ( 'NONE', *, *, #4989, .T. ) ;
#6923=CYLINDRICAL_SURFACE ( 'NONE', #2621, 0.7500000000000006661 ) ;
#6928=DIRECTION ( 'NONE',  ( 1.000000000000000000, 0.000000000000000000, -0.000000000000000000 ) ) ;
#6930=CARTESIAN_POINT ( 'NONE',  ( 79.82136590429890077, 114.1051029460540605, 10.00000000000000000 ) ) ;
#6933=CYLINDRICAL_SURFACE ( 'NONE', #2940, 0.7499999999999973355 ) ;
#6937=ORIENTED_EDGE ( 'NONE', *, *, #972, .T. ) ;
#6940=DIRECTION ( 'NONE',  ( -1.000000000000000000, 0.000000000000000000, 0.000000000000000000 ) ) ;
#6944=CIRCLE ( 'NONE', #8727, 9.999999999999994671 ) ;
#6945=( BOUNDED_CURVE ( )  B_SPLINE_CURVE ( 3, ( #6973, #13203, #620, #11251 ),
 .UNSPECIFIED., .F., .F. ) 
 B_SPLINE_CURVE_WITH_KNOTS ( ( 4, 4 ),
 ( 3.141592653589793116, 4.712388980384689674 ),
 .UNSPECIFIED. ) 
 CURVE ( )  GEOMETRIC_REPRESENTATION_ITEM ( )  RATIONAL_B_SPLINE_CURVE ( ( 1.000000000000000000, 0.8047378541243649375, 0.8047378541243649375, 1.000000000000000000 ) ) 
 REPRESENTATION_ITEM ( '' )  );
#6952=ADVANCED_FACE ( 'NONE', ( #7000 ), #6933, .T. ) ;
#6953=DIRECTION ( 'NONE',  ( 1.000000000000000000, 0.000000000000000000, 0.000000000000000000 ) ) ;
#6955=ORIENTED_EDGE ( 'NONE', *, *, #5607, .F. ) ;
#6956=CARTESIAN_POINT ( 'NONE',  ( 50.63563590245420443, 94.90549801902425031, 20.00000000000000000 ) ) ;
#6960=CARTESIAN_POINT ( 'NONE',  ( 42.94629607423402007, 110.9104019536709842, 20.00000000000000000 ) ) ;
#6962=DIRECTION ( 'NONE',  ( 0.000000000000000000, 0.000000000000000000, 1.000000000000000000 ) ) ;
#6966=CARTESIAN_POINT ( 'NONE',  ( 141.8856359024541973, 87.34974178189115435, 0.000000000000000000 ) ) ;
#6971=VERTEX_POINT ( 'NONE', #583 ) ;
#6973=CARTESIAN_POINT ( 'NONE',  ( 134.6356359024541973, 103.9054980190242361, 22.75000000000000000 ) ) ;
#6976=CARTESIAN_POINT ( 'NONE',  ( 113.0903281124166710, 100.8715034839261762, 10.00000000000000000 ) ) ;
#6977=EDGE_CURVE ( 'NONE', #5932, #8025, #1778, .T. ) ;
#6980=CARTESIAN_POINT ( 'NONE',  ( 76.11748380738829667, 82.61803701715820125, 20.00000000000000000 ) ) ;
#6982=ORIENTED_EDGE ( 'NONE', *, *, #5555, .F. ) ;
#6983=EDGE_CURVE ( 'NONE', #3980, #13266, #7064, .T. ) ;
#6984=ORIENTED_EDGE ( 'NONE', *, *, #636, .T. ) ;
#6986=VERTEX_POINT ( 'NONE', #4981 ) ;
#6994=CARTESIAN_POINT ( 'NONE',  ( 142.3249757306743675, 87.16776126655166479, 2.983588460272618114E-16 ) ) ;
#7000=FACE_OUTER_BOUND ( 'NONE', #12972, .T. ) ;
#7001=ORIENTED_EDGE ( 'NONE', *, *, #11759, .F. ) ;
#7005=DIRECTION ( 'NONE',  ( 0.000000000000000000, 0.000000000000000000, 1.000000000000000000 ) ) ;
#7013=ORIENTED_EDGE ( 'NONE', *, *, #4413, .F. ) ;
#7016=DIRECTION ( 'NONE',  ( 0.000000000000000000, 0.000000000000000000, 1.000000000000000000 ) ) ;
#7019=FACE_OUTER_BOUND ( 'NONE', #10366, .T. ) ;
#7020=DIRECTION ( 'NONE',  ( -1.000000000000000000, 0.000000000000000000, 0.000000000000000000 ) ) ;
#7023=CARTESIAN_POINT ( 'NONE',  ( 43.38563590245419732, 110.7284214383315089, 20.00000000000000000 ) ) ;
#7025=DIRECTION ( 'NONE',  ( 1.000000000000000000, -0.000000000000000000, 0.000000000000000000 ) ) ;
#7027=CARTESIAN_POINT ( 'NONE',  ( 92.63563590245421153, 99.03908161011133870, 20.00000000000000000 ) ) ;
#7031=EDGE_CURVE ( 'NONE', #4495, #9970, #8095, .T. ) ;
#7032=EDGE_LOOP ( 'NONE', ( #10004, #11262, #9503, #11571 ) ) ;
#7041=CARTESIAN_POINT ( 'NONE',  ( 134.6356359024541973, 108.9054980190242503, 22.75000000000000000 ) ) ;
#7045=CARTESIAN_POINT ( 'NONE',  ( 42.63563590245419732, 85.03908161011133870, 20.00000000000000000 ) ) ;
#7064=LINE ( 'NONE', #11339, #12948 ) ;
#7067=EDGE_CURVE ( 'NONE', #2183, #4982, #9580, .T. ) ;
#7072=CARTESIAN_POINT ( 'NONE',  ( 50.63563590245420443, 89.90549801902423610, 20.00000000000000000 ) ) ;
#7082=AXIS2_PLACEMENT_3D ( 'NONE', #6825, #7797, #12149 ) ;
#7085=CARTESIAN_POINT ( 'NONE',  ( 50.63563590245420443, 89.90549801902423610, 22.89644660940672694 ) ) ;
#7089=CARTESIAN_POINT ( 'NONE',  ( 76.18094369249178044, 97.20665973629650125, 20.00000000000000000 ) ) ;
#7090=CARTESIAN_POINT ( 'NONE',  ( 142.6356359024541973, 111.0390816101113245, 0.7500000000000006661 ) ) ;
#7091=PLANE ( 'NONE',  #2912 ) ;
#7092=DIRECTION ( 'NONE',  ( 1.000000000000000000, 0.000000000000000000, 0.000000000000000000 ) ) ;
#7096=CIRCLE ( 'NONE', #2218, 9.999999999999994671 ) ;
#7100=PRODUCT_DEFINITION_CONTEXT ( 'detailed design', #6886, 'design' ) ;
#7107=VECTOR ( 'NONE', #1877, 1000.000000000000000 ) ;
#7111=CARTESIAN_POINT ( 'NONE',  ( 134.8856359024541973, 94.65549801902425031, 23.00000000000000000 ) ) ;
#7118=ORIENTED_EDGE ( 'NONE', *, *, #6132, .F. ) ;
#7126=CARTESIAN_POINT ( 'NONE',  ( 141.8856359024541973, 87.34974178189115435, 0.000000000000000000 ) ) ;
#7137=VECTOR ( 'NONE', #1305, 1000.000000000000000 ) ;
#7149=DIRECTION ( 'NONE',  ( 0.000000000000000000, 0.000000000000000000, 1.000000000000000000 ) ) ;
#7150=EDGE_CURVE ( 'NONE', #2952, #9710, #3107, .T. ) ;
#7152=CIRCLE ( 'NONE', #3822, 0.7500000000000006661 ) ;
#7157=CARTESIAN_POINT ( 'NONE',  ( 140.3249757306743675, 112.2890816101113387, 0.000000000000000000 ) ) ;
#7158=AXIS2_PLACEMENT_3D ( 'NONE', #11500, #2938, #7163 ) ;
#7161=CARTESIAN_POINT ( 'NONE',  ( 141.8856359024541973, 87.34974178189115435, 20.00000000000000000 ) ) ;
#7163=DIRECTION ( 'NONE',  ( 0.000000000000000000, -0.000000000000000000, -1.000000000000000000 ) ) ;
#7171=VERTEX_POINT ( 'NONE', #10002 ) ;
#7174=DIRECTION ( 'NONE',  ( 0.000000000000000000, 0.000000000000000000, 1.000000000000000000 ) ) ;
#7181=LINE ( 'NONE', #11459, #10709 ) ;
#7191=CARTESIAN_POINT ( 'NONE',  ( 98.63563590245422574, 99.03908161011133870, 0.000000000000000000 ) ) ;
#7193=ORIENTED_EDGE ( 'NONE', *, *, #12110, .T. ) ;
#7196=CARTESIAN_POINT ( 'NONE',  ( 185.2712718049083946, 94.65549801902425031, 23.00000000000000000 ) ) ;
#7198=PLANE ( 'NONE',  #4473 ) ;
#7199=EDGE_CURVE ( 'NONE', #8025, #6125, #7669, .T. ) ;
#7200=ORIENTED_EDGE ( 'NONE', *, *, #1698, .T. ) ;
#7201=ADVANCED_FACE ( 'NONE', ( #9721 ), #8879, .T. ) ;
#7208=DIRECTION ( 'NONE',  ( 1.000000000000000000, 0.000000000000000000, 0.000000000000000000 ) ) ;
#7217=CARTESIAN_POINT ( 'NONE',  ( 140.6356359024541973, 113.0390816101113387, 0.7500000000000006661 ) ) ;
#7224=DIRECTION ( 'NONE',  ( 1.000000000000000000, 0.000000000000000000, -0.000000000000000000 ) ) ;
#7228=DIRECTION ( 'NONE',  ( -0.000000000000000000, 1.000000000000000000, -0.000000000000000000 ) ) ;
#7231=ORIENTED_EDGE ( 'NONE', *, *, #6900, .T. ) ;
#7233=CARTESIAN_POINT ( 'NONE',  ( 44.63563590245420443, 89.90549801902423610, 22.75000000000000000 ) ) ;
#7238=CARTESIAN_POINT ( 'NONE',  ( 140.3249757306743675, 85.78908161011133870, 0.000000000000000000 ) ) ;
#7241=AXIS2_PLACEMENT_3D ( 'NONE', #3342, #4327, #2314 ) ;
#7254=DIRECTION ( 'NONE',  ( 0.000000000000000000, 0.000000000000000000, 1.000000000000000000 ) ) ;
#7266=EDGE_CURVE ( 'NONE', #4150, #6531, #3586, .T. ) ;
#7267=FACE_OUTER_BOUND ( 'NONE', #10886, .T. ) ;
#7278=CARTESIAN_POINT ( 'NONE',  ( 140.6356359024541973, 113.0390816101113387, 19.68933982822018081 ) ) ;
#7281=DIRECTION ( 'NONE',  ( 0.000000000000000000, 0.000000000000000000, 1.000000000000000000 ) ) ;
#7282=ADVANCED_FACE ( 'NONE', ( #3654 ), #8664, .F. ) ;
#7283=DIRECTION ( 'NONE',  ( 0.000000000000000000, -1.000000000000000000, 0.000000000000000000 ) ) ;
#7285=CARTESIAN_POINT ( 'NONE',  ( 82.99521369064696330, 82.14063840035363739, 20.00000000000000000 ) ) ;
#7300=ADVANCED_FACE ( 'NONE', ( #2275 ), #6510, .F. ) ;
#7305=DIRECTION ( 'NONE',  ( 1.000000000000000000, 0.000000000000000000, 0.000000000000000000 ) ) ;
#7307=TOROIDAL_SURFACE ( 'NONE', #7082, 10.75000000000000000, 0.7500000000000000000 ) ;
#7311=ADVANCED_FACE ( 'NONE', ( #11955 ), #12314, .F. ) ;
#7313=AXIS2_PLACEMENT_3D ( 'NONE', #10278, #12576, #1747 ) ;
#7323=DIRECTION ( 'NONE',  ( 0.000000000000000000, 0.000000000000000000, -1.000000000000000000 ) ) ;
#7324=VERTEX_POINT ( 'NONE', #6980 ) ;
#7325=PLANE ( 'NONE',  #12014 ) ;
#7329=EDGE_CURVE ( 'NONE', #4150, #2636, #2613, .T. ) ;
#7330=CARTESIAN_POINT ( 'NONE',  ( 140.6356359024541973, 108.9054980190242503, 23.00000000000000000 ) ) ;
#7337=CARTESIAN_POINT ( 'NONE',  ( 134.6356359024541973, 103.9054980190242361, 20.00000000000000000 ) ) ;
#7342=CARTESIAN_POINT ( 'NONE',  ( 92.63563590245421153, 99.03908161011133870, 19.25000000000000000 ) ) ;
#7345=CIRCLE ( 'NONE', #4472, 0.7500000000000000000 ) ;
#7348=ADVANCED_FACE ( 'NONE', ( #3922 ), #4965, .F. ) ;
#7350=CARTESIAN_POINT ( 'NONE',  ( 140.3249757306743675, 112.2890816101113387, 20.00000000000000000 ) ) ;
#7351=CYLINDRICAL_SURFACE ( 'NONE', #5554, 2.000000000000001776 ) ;
#7368=CIRCLE ( 'NONE', #11412, 24.04163056034261459 ) ;
#7370=LINE ( 'NONE', #4459, #6133 ) ;
#7373=ORIENTED_EDGE ( 'NONE', *, *, #7548, .T. ) ;
#7382=ORIENTED_EDGE ( 'NONE', *, *, #8126, .T. ) ;
#7387=EDGE_LOOP ( 'NONE', ( #5784, #12588, #6710, #10607 ) ) ;
#7388=LINE ( 'NONE', #1902, #9512 ) ;
#7391=CARTESIAN_POINT ( 'NONE',  ( 134.6356359024541973, 94.90549801902425031, 20.00000000000000000 ) ) ;
#7392=CARTESIAN_POINT ( 'NONE',  ( 76.11748380738829667, 115.4601262030644762, 0.000000000000000000 ) ) ;
#7394=LINE ( 'NONE', #11810, #1320 ) ;
#7398=ORIENTED_EDGE ( 'NONE', *, *, #3531, .F. ) ;
#7421=DIRECTION ( 'NONE',  ( -0.7071067811865520136, 0.7071067811865429098, 0.000000000000000000 ) ) ;
#7423=CARTESIAN_POINT ( 'NONE',  ( 140.3856359024541973, 0.000000000000000000, 22.75000000000000000 ) ) ;
#7424=ORIENTED_EDGE ( 'NONE', *, *, #11445, .T. ) ;
#7426=DIRECTION ( 'NONE',  ( 0.000000000000000000, 1.000000000000000000, 0.000000000000000000 ) ) ;
#7460=FACE_OUTER_BOUND ( 'NONE', #11214, .T. ) ;
#7464=DIRECTION ( 'NONE',  ( -1.000000000000000000, 0.000000000000000000, 0.000000000000000000 ) ) ;
#7466=CARTESIAN_POINT ( 'NONE',  ( 140.6356359024541689, 85.78908161011133870, 20.00000000000000000 ) ) ;
#7468=EDGE_CURVE ( 'NONE', #12568, #54, #8600, .T. ) ;
#7470=ADVANCED_FACE ( 'NONE', ( #81 ), #10848, .T. ) ;
#7476=DIRECTION ( 'NONE',  ( -0.000000000000000000, -0.000000000000000000, -1.000000000000000000 ) ) ;
#7481=ORIENTED_EDGE ( 'NONE', *, *, #5350, .F. ) ;
#7485=CIRCLE ( 'NONE', #11087, 2.000000000000001776 ) ;
#7489=ORIENTED_EDGE ( 'NONE', *, *, #11105, .F. ) ;
#7490=VECTOR ( 'NONE', #11295, 1000.000000000000000 ) ;
#7491=ORIENTED_EDGE ( 'NONE', *, *, #10576, .F. ) ;
#7495=ORIENTED_EDGE ( 'NONE', *, *, #11585, .T. ) ;
#7503=CIRCLE ( 'NONE', #11325, 0.7499999999999966693 ) ;
#7509=CARTESIAN_POINT ( 'NONE',  ( 109.0903281124166710, 100.8715034839261762, 10.00000000000000000 ) ) ;
#7519=CARTESIAN_POINT ( 'NONE',  ( 111.0903281124166710, 100.8715034839261762, 10.00000000000000000 ) ) ;
#7520=CARTESIAN_POINT ( 'NONE',  ( 68.49370948373500312, 112.2890816101113387, 0.000000000000000000 ) ) ;
#7521=DIRECTION ( 'NONE',  ( 0.000000000000000000, 1.000000000000000000, -0.000000000000000000 ) ) ;
#7525=VECTOR ( 'NONE', #10737, 1000.000000000000000 ) ;
#7533=ORIENTED_EDGE ( 'NONE', *, *, #9078, .F. ) ;
#7537=FACE_OUTER_BOUND ( 'NONE', #12770, .T. ) ;
#7544=AXIS2_PLACEMENT_3D ( 'NONE', #9744, #8417, #8693 ) ;
#7546=DIRECTION ( 'NONE',  ( 1.000000000000000000, 0.000000000000000000, 0.000000000000000000 ) ) ;
#7547=ORIENTED_EDGE ( 'NONE', *, *, #7548, .F. ) ;
#7548=EDGE_CURVE ( 'NONE', #12198, #4364, #3902, .T. ) ;
#7556=LINE ( 'NONE', #10868, #11983 ) ;
#7558=EDGE_CURVE ( 'NONE', #6706, #12630, #5446, .T. ) ;
#7560=CARTESIAN_POINT ( 'NONE',  ( 86.63563590245421153, 99.03908161011133870, 0.000000000000000000 ) ) ;
#7567=AXIS2_PLACEMENT_3D ( 'NONE', #9528, #2289, #9470 ) ;
#7570=ORIENTED_EDGE ( 'NONE', *, *, #12942, .T. ) ;
#7571=ORIENTED_EDGE ( 'NONE', *, *, #11990, .F. ) ;
#7577=AXIS2_PLACEMENT_3D ( 'NONE', #13559, #4840, #3873 ) ;
#7585=DIRECTION ( 'NONE',  ( -0.7071067811865451302, 0.7071067811865500152, -0.000000000000000000 ) ) ;
#7589=VECTOR ( 'NONE', #6218, 1000.000000000000000 ) ;
#7598=AXIS2_PLACEMENT_3D ( 'NONE', #11353, #13649, #10306 ) ;
#7599=CIRCLE ( 'NONE', #10746, 0.7499999999999966693 ) ;
#7601=DIRECTION ( 'NONE',  ( -1.000000000000000000, 0.000000000000000000, 0.000000000000000000 ) ) ;
#7602=CARTESIAN_POINT ( 'NONE',  ( 75.58559257550551536, 115.9888905337886769, 20.00000000000000000 ) ) ;
#7606=ORIENTED_EDGE ( 'NONE', *, *, #10444, .F. ) ;
#7609=CARTESIAN_POINT ( 'NONE',  ( 50.38563590245420443, 0.000000000000000000, 23.00000000000000000 ) ) ;
#7613=DIRECTION ( 'NONE',  ( -0.7071067811865425767, 0.7071067811865524577, 0.000000000000000000 ) ) ;
#7625=( BOUNDED_CURVE ( )  B_SPLINE_CURVE ( 3, ( #2860, #7085, #11364, #9539 ),
 .UNSPECIFIED., .F., .F. ) 
 B_SPLINE_CURVE_WITH_KNOTS ( ( 4, 4 ),
 ( 0.000000000000000000, 1.570796326794896558 ),
 .UNSPECIFIED. ) 
 CURVE ( )  GEOMETRIC_REPRESENTATION_ITEM ( )  RATIONAL_B_SPLINE_CURVE ( ( 1.000000000000000000, 0.8047378541243649375, 0.8047378541243649375, 1.000000000000000000 ) ) 
 REPRESENTATION_ITEM ( '' )  );
#7631=EDGE_LOOP ( 'NONE', ( #4062, #12220 ) ) ;
#7635=FILL_AREA_STYLE_COLOUR ( '', #1278 ) ;
#7638=DIRECTION ( 'NONE',  ( -0.7071067811865525687, -0.7071067811865425767, 0.000000000000000000 ) ) ;
#7639=FACE_OUTER_BOUND ( 'NONE', #13157, .T. ) ;
#7650=CARTESIAN_POINT ( 'NONE',  ( 140.6356359024541973, 94.90549801902423610, 22.89644660940672694 ) ) ;
#7653=LINE ( 'NONE', #11935, #5513 ) ;
#7657=LINE ( 'NONE', #1173, #5574 ) ;
#7664=ORIENTED_EDGE ( 'NONE', *, *, #12073, .T. ) ;
#7667=FACE_OUTER_BOUND ( 'NONE', #2955, .T. ) ;
#7669=LINE ( 'NONE', #8956, #6262 ) ;
#7673=ORIENTED_EDGE ( 'NONE', *, *, #10444, .T. ) ;
#7675=CARTESIAN_POINT ( 'NONE',  ( 141.8856359024541973, 110.7284214383315089, 20.00000000000000000 ) ) ;
#7680=CARTESIAN_POINT ( 'NONE',  ( 116.7775623211734342, 75.03908161011133870, 0.7500000000000006661 ) ) ;
#7683=CARTESIAN_POINT ( 'NONE',  ( 116.7775623211734342, 85.03908161011133870, 19.25000000000000000 ) ) ;
#7689=VERTEX_POINT ( 'NONE', #570 ) ;
#7690=ORIENTED_EDGE ( 'NONE', *, *, #13444, .F. ) ;
#7693=ORIENTED_EDGE ( 'NONE', *, *, #1447, .F. ) ;
#7704=FACE_OUTER_BOUND ( 'NONE', #13201, .T. ) ;
#7708=ORIENTED_EDGE ( 'NONE', *, *, #13635, .F. ) ;
#7713=DIRECTION ( 'NONE',  ( 1.000000000000000000, 0.000000000000000000, 0.000000000000000000 ) ) ;
#7715=VERTEX_POINT ( 'NONE', #13805 ) ;
#7725=EDGE_CURVE ( 'NONE', #9665, #217, #4342, .T. ) ;
#7729=VECTOR ( 'NONE', #6592, 1000.000000000000000 ) ;
#7732=ADVANCED_FACE ( 'NONE', ( #11107 ), #1669, .T. ) ;
#7733=EDGE_LOOP ( 'NONE', ( #8889, #8385 ) ) ;
#7738=DIRECTION ( 'NONE',  ( 1.000000000000000000, 0.000000000000000000, -0.000000000000000000 ) ) ;
#7743=EDGE_CURVE ( 'NONE', #1109, #12176, #9693, .T. ) ;
#7754=DIRECTION ( 'NONE',  ( -0.000000000000000000, 1.000000000000000000, -0.000000000000000000 ) ) ;
#7763=CARTESIAN_POINT ( 'NONE',  ( 44.63563590245420443, 103.9054980190242361, 22.75000000000000000 ) ) ;
#7765=AXIS2_PLACEMENT_3D ( 'NONE', #11333, #1840, #1767 ) ;
#7769=CARTESIAN_POINT ( 'NONE',  ( 100.2760581142613603, 115.9375248198690826, 10.00000000000000000 ) ) ;
#7775=ORIENTED_EDGE ( 'NONE', *, *, #10615, .T. ) ;
#7782=CARTESIAN_POINT ( 'NONE',  ( 185.2712718049083946, 108.6554980190242503, 23.00000000000000000 ) ) ;
#7786=CIRCLE ( 'NONE', #10044, 10.74999999999999645 ) ;
#7788=CARTESIAN_POINT ( 'NONE',  ( 98.63563590245422574, 99.03908161011133870, 20.00000000000000000 ) ) ;
#7793=VECTOR ( 'NONE', #10911, 1000.000000000000000 ) ;
#7797=DIRECTION ( 'NONE',  ( 0.000000000000000000, 0.000000000000000000, 1.000000000000000000 ) ) ;
#7803=TOROIDAL_SURFACE ( 'NONE', #6476, 10.75000000000000000, 0.7500000000000000000 ) ;
#7805=VECTOR ( 'NONE', #10498, 1000.000000000000000 ) ;
#7812=CARTESIAN_POINT ( 'NONE',  ( 44.88563590245420443, 108.6554980190242503, 23.00000000000000000 ) ) ;
#7814=AXIS2_PLACEMENT_3D ( 'NONE', #8419, #3268, #11768 ) ;
#7819=CARTESIAN_POINT ( 'NONE',  ( 44.63563590245420443, 89.90549801902423610, 23.00000000000000000 ) ) ;
#7820=EDGE_CURVE ( 'NONE', #12394, #7171, #8945, .T. ) ;
#7821=VERTEX_POINT ( 'NONE', #5712 ) ;
#7829=ORIENTED_EDGE ( 'NONE', *, *, #10744, .T. ) ;
#7830=EDGE_LOOP ( 'NONE', ( #2053, #13619, #9943, #8129 ) ) ;
#7847=FACE_OUTER_BOUND ( 'NONE', #996, .T. ) ;
#7852=DIRECTION ( 'NONE',  ( 0.000000000000000000, 0.000000000000000000, 1.000000000000000000 ) ) ;
#7857=VECTOR ( 'NONE', #2995, 1000.000000000000000 ) ;
#7858=EDGE_CURVE ( 'NONE', #11822, #7715, #8304, .T. ) ;
#7864=CARTESIAN_POINT ( 'NONE',  ( 44.76431555889458735, 112.7284214383315089, 20.00000000000000000 ) ) ;
#7870=CARTESIAN_POINT ( 'NONE',  ( 44.88563590245420443, 94.90549801902425031, 22.75000000000000000 ) ) ;
#7871=CARTESIAN_POINT ( 'NONE',  ( 140.6356359024541973, 108.9054980190242503, 22.75000000000000000 ) ) ;
#7874=CIRCLE ( 'NONE', #4234, 24.04163056034261459 ) ;
#7886=VERTEX_POINT ( 'NONE', #818 ) ;
#7888=FACE_OUTER_BOUND ( 'NONE', #10286, .T. ) ;
#7889=LINE ( 'NONE', #8877, #10055 ) ;
#7902=EDGE_CURVE ( 'NONE', #12702, #4150, #8909, .T. ) ;
#7907=EDGE_CURVE ( 'NONE', #8675, #13218, #10395, .T. ) ;
#7912=EDGE_CURVE ( 'NONE', #10620, #12198, #5083, .T. ) ;
#7914=DIRECTION ( 'NONE',  ( 0.000000000000000000, 0.000000000000000000, 1.000000000000000000 ) ) ;
#7926=EDGE_CURVE ( 'NONE', #6706, #4329, #5243, .T. ) ;
#7928=DIRECTION ( 'NONE',  ( 0.000000000000000000, 0.000000000000000000, 1.000000000000000000 ) ) ;
#7934=DIRECTION ( 'NONE',  ( -0.7071067811865474617, -0.7071067811865474617, 0.000000000000000000 ) ) ;
#7935=FACE_OUTER_BOUND ( 'NONE', #3435, .T. ) ;
#7937=LINE ( 'NONE', #2596, #1299 ) ;
#7939=AXIS2_PLACEMENT_3D ( 'NONE', #13363, #10412, #3098 ) ;
#7941=DIRECTION ( 'NONE',  ( 0.000000000000000000, 1.000000000000000000, 0.000000000000000000 ) ) ;
#7942=CARTESIAN_POINT ( 'NONE',  ( 44.76431555889458735, 112.7284214383315089, 3.521624574640407997E-16 ) ) ;
#7944=VERTEX_POINT ( 'NONE', #3912 ) ;
#7945=VECTOR ( 'NONE', #10205, 1000.000000000000000 ) ;
#7946=DIRECTION ( 'NONE',  ( -1.000000000000000000, 0.000000000000000000, 0.000000000000000000 ) ) ;
#7952=DIRECTION ( 'NONE',  ( -0.000000000000000000, -0.000000000000000000, -1.000000000000000000 ) ) ;
#7955=VECTOR ( 'NONE', #12352, 1000.000000000000000 ) ;
#7958=ORIENTED_EDGE ( 'NONE', *, *, #730, .T. ) ;
#7963=ORIENTED_EDGE ( 'NONE', *, *, #3553, .T. ) ;
#7966=ORIENTED_EDGE ( 'NONE', *, *, #13296, .F. ) ;
#7967=CARTESIAN_POINT ( 'NONE',  ( 140.6356359024541973, 94.90549801902425031, 23.00000000000000000 ) ) ;
#7975=ADVANCED_FACE ( 'NONE', ( #2102 ), #3278, .T. ) ;
#7984=EDGE_CURVE ( 'NONE', #11929, #6593, #11319, .T. ) ;
#7988=AXIS2_PLACEMENT_3D ( 'NONE', #2818, #13410, #4066 ) ;
#7992=CARTESIAN_POINT ( 'NONE',  ( 185.2712718049083946, 0.000000000000000000, 23.00000000000000000 ) ) ;
#7993=CARTESIAN_POINT ( 'NONE',  ( 81.82136590429890077, 114.1051029460540605, 10.00000000000000000 ) ) ;
#7996=FACE_BOUND ( 'NONE', #2695, .T. ) ;
#7998=EDGE_CURVE ( 'NONE', #5796, #12702, #2237, .T. ) ;
#8001=CIRCLE ( 'NONE', #4223, 2.000000000000001776 ) ;
#8010=ADVANCED_FACE ( 'NONE', ( #2808 ), #8153, .F. ) ;
#8013=CARTESIAN_POINT ( 'NONE',  ( 140.3249757306743675, 112.2890816101113387, 0.000000000000000000 ) ) ;
#8014=FACE_OUTER_BOUND ( 'NONE', #2241, .T. ) ;
#8015=CARTESIAN_POINT ( 'NONE',  ( 142.6356359024541973, 111.0390816101113103, 0.3106601717798236351 ) ) ;
#8025=VERTEX_POINT ( 'NONE', #1229 ) ;
#8040=ORIENTED_EDGE ( 'NONE', *, *, #13308, .F. ) ;
#8042=AXIS2_PLACEMENT_3D ( 'NONE', #1256, #10772, #6633 ) ;
#8053=AXIS2_PLACEMENT_3D ( 'NONE', #3505, #12090, #5650 ) ;
#8056=VECTOR ( 'NONE', #3210, 1000.000000000000114 ) ;
#8058=ORIENTED_EDGE ( 'NONE', *, *, #11732, .T. ) ;
#8060=ORIENTED_EDGE ( 'NONE', *, *, #5245, .T. ) ;
#8063=EDGE_CURVE ( 'NONE', #5932, #939, #7370, .T. ) ;
#8068=AXIS2_PLACEMENT_3D ( 'NONE', #2425, #13151, #12177 ) ;
#8070=AXIS2_PLACEMENT_3D ( 'NONE', #8759, #4368, #6525 ) ;
#8072=FACE_OUTER_BOUND ( 'NONE', #4205, .T. ) ;
#8077=DIRECTION ( 'NONE',  ( 1.000000000000000000, 0.000000000000000000, 0.000000000000000000 ) ) ;
#8085=DIRECTION ( 'NONE',  ( -0.7071067811865451302, 0.7071067811865500152, -0.000000000000000000 ) ) ;
#8091=CARTESIAN_POINT ( 'NONE',  ( 42.63563590245419732, 113.0390816101113387, 20.00000000000000000 ) ) ;
#8095=( BOUNDED_CURVE ( )  B_SPLINE_CURVE ( 3, ( #1632, #5882, #1697, #5942 ),
 .UNSPECIFIED., .F., .F. ) 
 B_SPLINE_CURVE_WITH_KNOTS ( ( 4, 4 ),
 ( 1.570796326794896558, 3.141592653589793116 ),
 .UNSPECIFIED. ) 
 CURVE ( )  GEOMETRIC_REPRESENTATION_ITEM ( )  RATIONAL_B_SPLINE_CURVE ( ( 1.000000000000000000, 0.8047378541243649375, 0.8047378541243649375, 1.000000000000000000 ) ) 
 REPRESENTATION_ITEM ( '' )  );
#8098=CARTESIAN_POINT ( 'NONE',  ( 42.63563590245419732, 87.03908161011136713, 20.00000000000000000 ) ) ;
#8100=ORIENTED_EDGE ( 'NONE', *, *, #3063, .T. ) ;
#8104=DIRECTION ( 'NONE',  ( 0.000000000000000000, -1.000000000000000000, 0.000000000000000000 ) ) ;
#8110=CARTESIAN_POINT ( 'NONE',  ( 44.63563590245420443, 94.90549801902425031, 22.75000000000000000 ) ) ;
#8112=ORIENTED_EDGE ( 'NONE', *, *, #9078, .T. ) ;
#8116=ORIENTED_EDGE ( 'NONE', *, *, #9831, .T. ) ;
#8121=CARTESIAN_POINT ( 'NONE',  ( 50.63563590245420443, 94.90549801902425031, 23.00000000000000000 ) ) ;
#8124=DIRECTION ( 'NONE',  ( 1.000000000000000000, 0.000000000000000000, 0.000000000000000000 ) ) ;
#8126=EDGE_CURVE ( 'NONE', #1567, #2972, #4668, .T. ) ;
#8129=ORIENTED_EDGE ( 'NONE', *, *, #1897, .F. ) ;
#8132=CARTESIAN_POINT ( 'NONE',  ( 116.7775623211734342, 75.03908161011133870, 0.000000000000000000 ) ) ;
#8135=CARTESIAN_POINT ( 'NONE',  ( 92.63563590245421153, 99.03908161011133870, 20.00000000000000000 ) ) ;
#8141=AXIS2_PLACEMENT_3D ( 'NONE', #5924, #5998, #11259 ) ;
#8150=FACE_OUTER_BOUND ( 'NONE', #8601, .T. ) ;
#8152=DIRECTION ( 'NONE',  ( 0.000000000000000000, 0.000000000000000000, 1.000000000000000000 ) ) ;
#8153=CYLINDRICAL_SURFACE ( 'NONE', #1297, 2.000000000000001776 ) ;
#8156=EDGE_CURVE ( 'NONE', #13231, #3610, #2163, .T. ) ;
#8160=ORIENTED_EDGE ( 'NONE', *, *, #10346, .T. ) ;
#8165=CIRCLE ( 'NONE', #12837, 23.29163056034261459 ) ;
#8168=CARTESIAN_POINT ( 'NONE',  ( 43.38563590245419732, 110.7284214383315089, 0.000000000000000000 ) ) ;
#8169=DIRECTION ( 'NONE',  ( -1.000000000000000000, 0.000000000000000000, -0.000000000000000000 ) ) ;
#8170=CARTESIAN_POINT ( 'NONE',  ( 50.63563590245420443, 90.15549801902423610, 22.75000000000000000 ) ) ;
#8180=DIRECTION ( 'NONE',  ( -0.7091883091770476710, -0.7050191076322684935, 0.000000000000000000 ) ) ;
#8181=CARTESIAN_POINT ( 'NONE',  ( 142.6356359024541973, 87.03908161011133870, 0.3106601717798216367 ) ) ;
#8185=DIRECTION ( 'NONE',  ( 0.000000000000000000, 0.000000000000000000, 1.000000000000000000 ) ) ;
#8195=PLANE ( 'NONE',  #6639 ) ;
#8197=AXIS2_PLACEMENT_3D ( 'NONE', #11831, #13651, #8546 ) ;
#8200=LINE ( 'NONE', #6163, #3528 ) ;
#8208=AXIS2_PLACEMENT_3D ( 'NONE', #9054, #4152, #5249 ) ;
#8209=VECTOR ( 'NONE', #13611, 1000.000000000000000 ) ;
#8211=CARTESIAN_POINT ( 'NONE',  ( 140.5069562460138286, 112.7284214383315089, 4.059660689008197386E-16 ) ) ;
#8217=DIRECTION ( 'NONE',  ( 0.000000000000000000, 0.000000000000000000, 1.000000000000000000 ) ) ;
#8218=CARTESIAN_POINT ( 'NONE',  ( 68.49370948373500312, 112.2890816101113387, 20.00000000000000000 ) ) ;
#8219=DIRECTION ( 'NONE',  ( 1.000000000000000000, 0.000000000000000000, 0.000000000000000000 ) ) ;
#8222=CARTESIAN_POINT ( 'NONE',  ( 140.3856359024541973, 108.6554980190242503, 23.00000000000000000 ) ) ;
#8227=AXIS2_PLACEMENT_3D ( 'NONE', #10809, #7426, #1221 ) ;
#8233=ORIENTED_EDGE ( 'NONE', *, *, #11878, .T. ) ;
#8235=CARTESIAN_POINT ( 'NONE',  ( 84.99521369064696330, 82.14063840035363739, 20.00000000000000000 ) ) ;
#8238=CARTESIAN_POINT ( 'NONE',  ( 116.7775623211734342, 75.03908161011133870, 19.25000000000000000 ) ) ;
#8240=CIRCLE ( 'NONE', #7544, 2.000000000000001776 ) ;
#8243=DIRECTION ( 'NONE',  ( 1.000000000000000000, 0.000000000000000000, -0.000000000000000000 ) ) ;
#8246=ORIENTED_EDGE ( 'NONE', *, *, #2449, .F. ) ;
#8252=DIRECTION ( 'NONE',  ( 0.000000000000000000, -1.000000000000000000, 0.000000000000000000 ) ) ;
#8257=ORIENTED_EDGE ( 'NONE', *, *, #1310, .F. ) ;
#8259=AXIS2_PLACEMENT_3D ( 'NONE', #3653, #13207, #5652 ) ;
#8260=CARTESIAN_POINT ( 'NONE',  ( 44.88563590245420443, 94.65549801902425031, 23.00000000000000000 ) ) ;
#8264=DIRECTION ( 'NONE',  ( 0.000000000000000000, -1.000000000000000000, 0.000000000000000000 ) ) ;
#8265=EDGE_CURVE ( 'NONE', #11879, #12380, #347, .T. ) ;
#8266=VECTOR ( 'NONE', #4534, 1000.000000000000000 ) ;
#8273=ADVANCED_FACE ( 'NONE', ( #5692 ), #600, .F. ) ;
#8274=FACE_OUTER_BOUND ( 'NONE', #8883, .T. ) ;
#8278=CARTESIAN_POINT ( 'NONE',  ( 44.63563590245420443, 89.90549801902423610, 20.00000000000000000 ) ) ;
#8280=VECTOR ( 'NONE', #12429, 1000.000000000000000 ) ;
#8282=VERTEX_POINT ( 'NONE', #6105 ) ;
#8296=CARTESIAN_POINT ( 'NONE',  ( 68.49370948373500312, 75.03908161011133870, 19.25000000000000000 ) ) ;
#8304=LINE ( 'NONE', #8098, #786 ) ;
#8306=ORIENTED_EDGE ( 'NONE', *, *, #12611, .F. ) ;
#8313=EDGE_CURVE ( 'NONE', #4612, #10749, #5465, .T. ) ;
#8314=ADVANCED_FACE ( 'NONE', ( #3957 ), #5964, .F. ) ;
#8315=ORIENTED_EDGE ( 'NONE', *, *, #1897, .T. ) ;
#8325=ORIENTED_EDGE ( 'NONE', *, *, #7907, .T. ) ;
#8327=DIRECTION ( 'NONE',  ( 1.000000000000000000, -0.000000000000000000, -0.000000000000000000 ) ) ;
#8334=ORIENTED_EDGE ( 'NONE', *, *, #9444, .T. ) ;
#8338=ORIENTED_EDGE ( 'NONE', *, *, #2449, .T. ) ;
#8339=EDGE_CURVE ( 'NONE', #5130, #11676, #8382, .T. ) ;
#8342=DIRECTION ( 'NONE',  ( -0.000000000000000000, -1.000000000000000000, -0.000000000000000000 ) ) ;
#8344=DIRECTION ( 'NONE',  ( 0.000000000000000000, 0.000000000000000000, 1.000000000000000000 ) ) ;
#8349=ORIENTED_EDGE ( 'NONE', *, *, #13449, .F. ) ;
#8355=CARTESIAN_POINT ( 'NONE',  ( 50.63563590245420443, 89.90549801902423610, 22.75000000000000000 ) ) ;
#8360=CARTESIAN_POINT ( 'NONE',  ( 44.88563590245420443, 104.1554980190242361, 23.00000000000000000 ) ) ;
#8369=DIRECTION ( 'NONE',  ( 0.000000000000000000, 0.000000000000000000, 1.000000000000000000 ) ) ;
#8371=CLOSED_SHELL ( 'NONE', ( #8010, #8445, #1331, #12490, #8542, #205, #1314, #6460, #10030, #1616, #7732, #6088, #7311, #8563, #11991, #8314, #9948, #1504, #6627, #8273, #7348, #4271, #11154, #11343, #3196, #4433, #12801, #10406, #6588, #3262, #11260, #1732, #12269, #7975, #7470, #3778, #3992, #3573, #11817, #5558, #247, #6204, #4016, #4701, #6952, #10799, #4510, #1885, #5619, #12346, #11992, #629, #6799, #9591, #10003, #13067, #1131, #950, #6781, #465, #7282, #11793, #650, #12795, #128, #13529, #7300, #1365, #1627, #9298, #10742, #5872, #10828, #1176, #2112, #3335, #10285, #11627, #6883, #9729, #4338, #5117, #1988, #11420, #13438, #3194, #12704, #9628, #11560, #3133, #8763, #6693, #5361, #13322, #5434, #7201, #9432, #2477, #12577, #13102, #1700, #4340, #8795, #13091, #12307, #3399 ) ) ;
#8372=ORIENTED_EDGE ( 'NONE', *, *, #2635, .F. ) ;
#8375=EDGE_CURVE ( 'NONE', #4458, #2858, #1650, .T. ) ;
#8379=( BOUNDED_CURVE ( )  B_SPLINE_CURVE ( 3, ( #13240, #3743, #2444, #5825 ),
 .UNSPECIFIED., .F., .F. ) 
 B_SPLINE_CURVE_WITH_KNOTS ( ( 4, 4 ),
 ( 0.000000000000000000, 1.570796326794896558 ),
 .UNSPECIFIED. ) 
 CURVE ( )  GEOMETRIC_REPRESENTATION_ITEM ( )  RATIONAL_B_SPLINE_CURVE ( ( 1.000000000000000000, 0.8047378541243649375, 0.8047378541243649375, 1.000000000000000000 ) ) 
 REPRESENTATION_ITEM ( '' )  );
#8382=CIRCLE ( 'NONE', #6813, 6.000000000000005329 ) ;
#8385=ORIENTED_EDGE ( 'NONE', *, *, #4696, .F. ) ;
#8388=FACE_OUTER_BOUND ( 'NONE', #7032, .T. ) ;
#8390=LINE ( 'NONE', #13625, #11847 ) ;
#8391=DIRECTION ( 'NONE',  ( 0.000000000000000000, 0.000000000000000000, 1.000000000000000000 ) ) ;
#8395=EDGE_CURVE ( 'NONE', #11676, #5130, #3939, .T. ) ;
#8399=ORIENTED_EDGE ( 'NONE', *, *, #2164, .F. ) ;
#8400=ORIENTED_EDGE ( 'NONE', *, *, #4090, .F. ) ;
#8402=CARTESIAN_POINT ( 'NONE',  ( 92.63563590245421153, 112.2890816101113387, 0.000000000000000000 ) ) ;
#8413=ORIENTED_EDGE ( 'NONE', *, *, #2752, .T. ) ;
#8415=CARTESIAN_POINT ( 'NONE',  ( 111.0903281124166710, 100.8715034839261762, 10.00000000000000000 ) ) ;
#8417=DIRECTION ( 'NONE',  ( 0.000000000000000000, 0.000000000000000000, 1.000000000000000000 ) ) ;
#8419=CARTESIAN_POINT ( 'NONE',  ( 43.38563590245419732, 99.03908161011133870, 19.25000000000000000 ) ) ;
#8427=DIRECTION ( 'NONE',  ( 1.000000000000000000, 0.000000000000000000, 0.000000000000000000 ) ) ;
#8429=DIRECTION ( 'NONE',  ( 0.000000000000000000, 0.000000000000000000, 1.000000000000000000 ) ) ;
#8439=DIRECTION ( 'NONE',  ( 0.000000000000000000, 0.000000000000000000, 1.000000000000000000 ) ) ;
#8441=CARTESIAN_POINT ( 'NONE',  ( 50.38563590245420443, 0.000000000000000000, 23.00000000000000000 ) ) ;
#8445=ADVANCED_FACE ( 'NONE', ( #8618 ), #5205, .F. ) ;
#8448=EDGE_LOOP ( 'NONE', ( #10671, #5556, #4870, #13469 ) ) ;
#8461=ORIENTED_EDGE ( 'NONE', *, *, #2404, .T. ) ;
#8464=EDGE_CURVE ( 'NONE', #12738, #11762, #10392, .T. ) ;
#8486=CARTESIAN_POINT ( 'NONE',  ( 44.94629607423404849, 85.78908161011133870, 0.000000000000000000 ) ) ;
#8489=FILL_AREA_STYLE ('',( #7635 ) ) ;
#8500=VECTOR ( 'NONE', #3962, 1000.000000000000000 ) ;
#8505=ORIENTED_EDGE ( 'NONE', *, *, #3531, .T. ) ;
#8506=ORIENTED_EDGE ( 'NONE', *, *, #9403, .F. ) ;
#8509=EDGE_CURVE ( 'NONE', #11762, #11089, #8165, .T. ) ;
#8516=EDGE_LOOP ( 'NONE', ( #3646, #1475 ) ) ;
#8518=VECTOR ( 'NONE', #8085, 1000.000000000000114 ) ;
#8524=CARTESIAN_POINT ( 'NONE',  ( 140.5320825118609207, 90.00905140961751272, 23.00000000000000000 ) ) ;
#8529=EDGE_CURVE ( 'NONE', #10620, #4458, #9972, .T. ) ;
#8542=ADVANCED_FACE ( 'NONE', ( #6254 ), #10524, .F. ) ;
#8546=DIRECTION ( 'NONE',  ( 0.000000000000000000, 0.000000000000000000, -1.000000000000000000 ) ) ;
#8547=CARTESIAN_POINT ( 'NONE',  ( 134.6356359024541973, 94.90549801902425031, 22.75000000000000000 ) ) ;
#8551=ORIENTED_EDGE ( 'NONE', *, *, #10486, .F. ) ;
#8552=DIRECTION ( 'NONE',  ( -0.000000000000000000, -0.000000000000000000, 1.000000000000000000 ) ) ;
#8554=CYLINDRICAL_SURFACE ( 'NONE', #5363, 0.7500000000000000000 ) ;
#8555=CARTESIAN_POINT ( 'NONE',  ( 109.0903281124166710, 100.8715034839261762, 10.00000000000000000 ) ) ;
#8556=CARTESIAN_POINT ( 'NONE',  ( 44.63563590245421153, 85.03908161011132449, 0.3106601717798216367 ) ) ;
#8563=ADVANCED_FACE ( 'NONE', ( #7847 ), #12122, .F. ) ;
#8567=CARTESIAN_POINT ( 'NONE',  ( 44.88563590245420443, 0.000000000000000000, 23.00000000000000000 ) ) ;
#8583=ORIENTED_EDGE ( 'NONE', *, *, #9742, .F. ) ;
#8588=ORIENTED_EDGE ( 'NONE', *, *, #10711, .T. ) ;
#8597=ORIENTED_EDGE ( 'NONE', *, *, #7858, .T. ) ;
#8599=ORIENTED_EDGE ( 'NONE', *, *, #8769, .T. ) ;
#8600=LINE ( 'NONE', #7609, #6361 ) ;
#8601=EDGE_LOOP ( 'NONE', ( #10034, #2625, #13688, #13655 ) ) ;
#8605=CARTESIAN_POINT ( 'NONE',  ( 44.63563590245420443, 108.9054980190242503, 22.75000000000000000 ) ) ;
#8612=EDGE_CURVE ( 'NONE', #13530, #6986, #10867, .T. ) ;
#8618=FACE_OUTER_BOUND ( 'NONE', #6045, .T. ) ;
#8621=CARTESIAN_POINT ( 'NONE',  ( 50.53208251186094202, 108.8019446284309737, 23.00000000000000000 ) ) ;
#8625=LINE ( 'NONE', #8700, #7525 ) ;
#8628=DIRECTION ( 'NONE',  ( 1.000000000000000000, 0.000000000000000000, 0.000000000000000000 ) ) ;
#8636=ORIENTED_EDGE ( 'NONE', *, *, #9034, .F. ) ;
#8646=VECTOR ( 'NONE', #9522, 1000.000000000000000 ) ;
#8650=AXIS2_PLACEMENT_3D ( 'NONE', #12432, #11595, #13613 ) ;
#8663=CARTESIAN_POINT ( 'NONE',  ( 50.63563590245420443, 94.90549801902425031, 23.00000000000000000 ) ) ;
#8664=CYLINDRICAL_SURFACE ( 'NONE', #1117, 2.000000000000001776 ) ;
#8675=VERTEX_POINT ( 'NONE', #5616 ) ;
#8685=AXIS2_PLACEMENT_3D ( 'NONE', #5543, #7476, #1285 ) ;
#8687=EDGE_CURVE ( 'NONE', #4490, #9992, #13637, .T. ) ;
#8690=ORIENTED_EDGE ( 'NONE', *, *, #816, .T. ) ;
#8693=DIRECTION ( 'NONE',  ( 1.000000000000000000, 0.000000000000000000, 0.000000000000000000 ) ) ;
#8696=CARTESIAN_POINT ( 'NONE',  ( 92.63563590245421153, 99.03908161011133870, -30.00000000000001776 ) ) ;
#8697=ORIENTED_EDGE ( 'NONE', *, *, #10576, .T. ) ;
#8700=CARTESIAN_POINT ( 'NONE',  ( 44.63563590245421864, 85.03908161011133870, 19.25000000000000000 ) ) ;
#8704=DIRECTION ( 'NONE',  ( -0.000000000000000000, -0.000000000000000000, -1.000000000000000000 ) ) ;
#8710=EDGE_LOOP ( 'NONE', ( #1369, #4107 ) ) ;
#8712=DIRECTION ( 'NONE',  ( -0.000000000000000000, -0.000000000000000000, -1.000000000000000000 ) ) ;
#8719=CARTESIAN_POINT ( 'NONE',  ( 81.82136590429890077, 114.1051029460540605, 10.00000000000000000 ) ) ;
#8720=CARTESIAN_POINT ( 'NONE',  ( 50.63563590245420443, 108.9054980190242503, 20.00000000000000000 ) ) ;
#8727=AXIS2_PLACEMENT_3D ( 'NONE', #8238, #11518, #9291 ) ;
#8730=VERTEX_POINT ( 'NONE', #9506 ) ;
#8737=CYLINDRICAL_SURFACE ( 'NONE', #10290, 0.2500000000000002220 ) ;
#8747=VERTEX_POINT ( 'NONE', #12514 ) ;
#8759=CARTESIAN_POINT ( 'NONE',  ( 116.7775623211734342, 123.0390816101113245, 0.7500000000000006661 ) ) ;
#8763=ADVANCED_FACE ( 'NONE', ( #8388 ), #13750, .T. ) ;
#8769=EDGE_CURVE ( 'NONE', #11310, #2183, #7388, .T. ) ;
#8778=LINE ( 'NONE', #262, #8056 ) ;
#8779=VECTOR ( 'NONE', #2982, 1000.000000000000000 ) ;
#8780=DIRECTION ( 'NONE',  ( -0.000000000000000000, -0.000000000000000000, -1.000000000000000000 ) ) ;
#8791=DIRECTION ( 'NONE',  ( 0.000000000000000000, 1.000000000000000000, -0.000000000000000000 ) ) ;
#8792=DIRECTION ( 'NONE',  ( -0.000000000000000000, -0.000000000000000000, -1.000000000000000000 ) ) ;
#8795=ADVANCED_FACE ( 'NONE', ( #9106 ), #12651, .T. ) ;
#8798=EDGE_CURVE ( 'NONE', #13076, #13640, #840, .T. ) ;
#8802=CARTESIAN_POINT ( 'NONE',  ( 109.1537879975201406, 115.4601262030644762, 0.7500000000000006661 ) ) ;
#8805=CYLINDRICAL_SURFACE ( 'NONE', #13138, 0.7500000000000072164 ) ;
#8810=VECTOR ( 'NONE', #5592, 1000.000000000000000 ) ;
#8815=ORIENTED_EDGE ( 'NONE', *, *, #6135, .F. ) ;
#8823=DIRECTION ( 'NONE',  ( -0.000000000000000000, -0.000000000000000000, 1.000000000000000000 ) ) ;
#8824=ORIENTED_EDGE ( 'NONE', *, *, #4989, .F. ) ;
#8835=VERTEX_POINT ( 'NONE', #989 ) ;
#8838=DIRECTION ( 'NONE',  ( -0.7091883091770476710, -0.7050191076322684935, 0.000000000000000000 ) ) ;
#8842=EDGE_LOOP ( 'NONE', ( #8869, #932, #5285, #12784 ) ) ;
#8849=DIRECTION ( 'NONE',  ( -1.000000000000000000, 0.000000000000000000, 0.000000000000000000 ) ) ;
#8855=ORIENTED_EDGE ( 'NONE', *, *, #4968, .T. ) ;
#8857=FACE_OUTER_BOUND ( 'NONE', #8448, .T. ) ;
#8858=DIRECTION ( 'NONE',  ( 1.000000000000000000, 0.000000000000000000, 0.000000000000000000 ) ) ;
#8859=EDGE_CURVE ( 'NONE', #13545, #10605, #5236, .T. ) ;
#8865=CARTESIAN_POINT ( 'NONE',  ( 42.63563590245419732, 111.0390816101113103, 0.3106601717798218587 ) ) ;
#8869=ORIENTED_EDGE ( 'NONE', *, *, #4879, .T. ) ;
#8871=CARTESIAN_POINT ( 'NONE',  ( 100.2760581142613603, 115.9375248198690826, 10.00000000000000000 ) ) ;
#8872=VECTOR ( 'NONE', #2356, 1000.000000000000000 ) ;
#8873=CARTESIAN_POINT ( 'NONE',  ( 92.63563590245421153, 112.2890816101113387, 19.25000000000000000 ) ) ;
#8875=DIRECTION ( 'NONE',  ( 1.000000000000000000, 0.000000000000000000, 0.000000000000000000 ) ) ;
#8877=CARTESIAN_POINT ( 'NONE',  ( 42.63563590245419732, 111.0390816101113387, 19.25000000000000000 ) ) ;
#8879=PLANE ( 'NONE',  #8042 ) ;
#8883=EDGE_LOOP ( 'NONE', ( #2184, #11692, #6576, #6195 ) ) ;
#8885=EDGE_LOOP ( 'NONE', ( #3034, #10105, #7547, #11212 ) ) ;
#8889=ORIENTED_EDGE ( 'NONE', *, *, #9178, .F. ) ;
#8891=CARTESIAN_POINT ( 'NONE',  ( 105.4499059006094654, 83.97306027416853169, 10.00000000000000000 ) ) ;
#8900=DIRECTION ( 'NONE',  ( 1.000000000000000000, 0.000000000000000000, 0.000000000000000000 ) ) ;
#8909=( BOUNDED_CURVE ( )  B_SPLINE_CURVE ( 3, ( #4888, #1736, #13533, #7233 ),
 .UNSPECIFIED., .F., .F. ) 
 B_SPLINE_CURVE_WITH_KNOTS ( ( 4, 4 ),
 ( 1.570796326794896558, 3.141592653589793116 ),
 .UNSPECIFIED. ) 
 CURVE ( )  GEOMETRIC_REPRESENTATION_ITEM ( )  RATIONAL_B_SPLINE_CURVE ( ( 1.000000000000000000, 0.8047378541243649375, 0.8047378541243649375, 1.000000000000000000 ) ) 
 REPRESENTATION_ITEM ( '' )  );
#8914=CARTESIAN_POINT ( 'NONE',  ( 86.63563590245421153, 99.03908161011133870, -30.00000000000001776 ) ) ;
#8926=PLANE ( 'NONE',  #1953 ) ;
#8929=AXIS2_PLACEMENT_3D ( 'NONE', #8170, #9075, #12374 ) ;
#8934=CARTESIAN_POINT ( 'NONE',  ( 134.8856359024541973, 0.000000000000000000, 22.75000000000000000 ) ) ;
#8939=AXIS2_PLACEMENT_3D ( 'NONE', #8871, #208, #7738 ) ;
#8941=EDGE_LOOP ( 'NONE', ( #8116, #13487 ) ) ;
#8944=VERTEX_POINT ( 'NONE', #9652 ) ;
#8945=LINE ( 'NONE', #9925, #355 ) ;
#8950=CARTESIAN_POINT ( 'NONE',  ( 140.5069562460138286, 85.34974178189114014, 2.445552345904828725E-16 ) ) ;
#8955=FACE_OUTER_BOUND ( 'NONE', #9671, .T. ) ;
#8956=CARTESIAN_POINT ( 'NONE',  ( 50.63563590245420443, 103.9054980190242361, 23.00000000000000000 ) ) ;
#8966=DIRECTION ( 'NONE',  ( -0.000000000000000000, -0.000000000000000000, -1.000000000000000000 ) ) ;
#8975=EDGE_CURVE ( 'NONE', #12380, #13076, #3580, .T. ) ;
#8977=ORIENTED_EDGE ( 'NONE', *, *, #4254, .F. ) ;
#8980=CARTESIAN_POINT ( 'NONE',  ( 44.63563590245419732, 108.9054980190242503, 22.89644660940672694 ) ) ;
#8982=DIRECTION ( 'NONE',  ( 1.000000000000000000, 0.000000000000000000, 0.000000000000000000 ) ) ;
#8991=( BOUNDED_CURVE ( )  B_SPLINE_CURVE ( 3, ( #7041, #10550, #12643, #4128 ),
 .UNSPECIFIED., .F., .F. ) 
 B_SPLINE_CURVE_WITH_KNOTS ( ( 4, 4 ),
 ( 0.000000000000000000, 1.570796326794896558 ),
 .UNSPECIFIED. ) 
 CURVE ( )  GEOMETRIC_REPRESENTATION_ITEM ( )  RATIONAL_B_SPLINE_CURVE ( ( 1.000000000000000000, 0.8047378541243649375, 0.8047378541243649375, 1.000000000000000000 ) ) 
 REPRESENTATION_ITEM ( '' )  );
#8994=ORIENTED_EDGE ( 'NONE', *, *, #4768, .F. ) ;
#8995=CARTESIAN_POINT ( 'NONE',  ( 50.63563590245420443, 108.9054980190242503, 22.75000000000000000 ) ) ;
#9004=FACE_OUTER_BOUND ( 'NONE', #10674, .T. ) ;
#9025=ORIENTED_EDGE ( 'NONE', *, *, #6115, .F. ) ;
#9028=CARTESIAN_POINT ( 'NONE',  ( 44.94629607423406270, 112.2890816101113387, 0.000000000000000000 ) ) ;
#9029=EDGE_CURVE ( 'NONE', #12630, #10544, #1039, .T. ) ;
#9030=ORIENTED_EDGE ( 'NONE', *, *, #5908, .F. ) ;
#9034=EDGE_CURVE ( 'NONE', #12138, #3128, #6774, .T. ) ;
#9040=PLANE ( 'NONE',  #2647 ) ;
#9042=VECTOR ( 'NONE', #9355, 1000.000000000000114 ) ;
#9054=CARTESIAN_POINT ( 'NONE',  ( 92.63563590245421153, 99.03908161011133870, 0.7500000000000006661 ) ) ;
#9060=VECTOR ( 'NONE', #3736, 1000.000000000000000 ) ;
#9063=ORIENTED_EDGE ( 'NONE', *, *, #12666, .F. ) ;
#9064=EDGE_CURVE ( 'NONE', #6077, #12460, #6945, .T. ) ;
#9072=LINE ( 'NONE', #357, #2962 ) ;
#9074=CARTESIAN_POINT ( 'NONE',  ( 86.63563590245421153, 99.03908161011133870, 20.00000000000000000 ) ) ;
#9075=DIRECTION ( 'NONE',  ( -1.000000000000000000, 0.000000000000000000, 0.000000000000000000 ) ) ;
#9076=VECTOR ( 'NONE', #6048, 1000.000000000000000 ) ;
#9078=EDGE_CURVE ( 'NONE', #6986, #3428, #3077, .T. ) ;
#9089=DIRECTION ( 'NONE',  ( -1.000000000000000000, 0.000000000000000000, 0.000000000000000000 ) ) ;
#9096=DIRECTION ( 'NONE',  ( 0.000000000000000000, -1.000000000000000000, 0.000000000000000000 ) ) ;
#9103=ORIENTED_EDGE ( 'NONE', *, *, #6239, .T. ) ;
#9106=FACE_OUTER_BOUND ( 'NONE', #12533, .T. ) ;
#9107=ORIENTED_EDGE ( 'NONE', *, *, #7725, .F. ) ;
#9118=DIRECTION ( 'NONE',  ( -0.000000000000000000, -0.000000000000000000, 1.000000000000000000 ) ) ;
#9122=VECTOR ( 'NONE', #5860, 1000.000000000000000 ) ;
#9123=CIRCLE ( 'NONE', #1533, 6.000000000000005329 ) ;
#9124=EDGE_CURVE ( 'NONE', #721, #5520, #12705, .T. ) ;
#9128=CARTESIAN_POINT ( 'NONE',  ( 81.82136590429890077, 114.1051029460540605, 20.00000000000000000 ) ) ;
#9129=ORIENTED_EDGE ( 'NONE', *, *, #5812, .F. ) ;
#9136=CARTESIAN_POINT ( 'NONE',  ( 72.18094369249178044, 97.20665973629650125, 20.00000000000000000 ) ) ;
#9152=CARTESIAN_POINT ( 'NONE',  ( 103.4499059006094512, 83.97306027416853169, 20.00000000000000000 ) ) ;
#9154=CARTESIAN_POINT ( 'NONE',  ( 103.4499059006094512, 83.97306027416853169, 10.00000000000000000 ) ) ;
#9155=DIRECTION ( 'NONE',  ( 0.000000000000000000, 1.000000000000000000, -0.000000000000000000 ) ) ;
#9158=FACE_OUTER_BOUND ( 'NONE', #1617, .T. ) ;
#9168=FACE_OUTER_BOUND ( 'NONE', #12118, .T. ) ;
#9171=ORIENTED_EDGE ( 'NONE', *, *, #8375, .T. ) ;
#9172=AXIS2_PLACEMENT_3D ( 'NONE', #4805, #5845, #8427 ) ;
#9177=CARTESIAN_POINT ( 'NONE',  ( 116.7775623211734342, 75.03908161011133870, 0.7500000000000006661 ) ) ;
#9178=EDGE_CURVE ( 'NONE', #13218, #1212, #7485, .T. ) ;
#9194=DIRECTION ( 'NONE',  ( 0.000000000000000000, 1.000000000000000000, 0.000000000000000000 ) ) ;
#9210=CARTESIAN_POINT ( 'NONE',  ( 44.63563590245419732, 103.9054980190242361, 22.89644660940672694 ) ) ;
#9214=EDGE_CURVE ( 'NONE', #11089, #8282, #6402, .T. ) ;
#9215=AXIS2_PLACEMENT_3D ( 'NONE', #7992, #5891, #10174 ) ;
#9221=EDGE_LOOP ( 'NONE', ( #1702, #13473, #8690, #1458 ) ) ;
#9230=PLANE ( 'NONE',  #10480 ) ;
#9249=CARTESIAN_POINT ( 'NONE',  ( 134.6356359024541973, 108.9054980190242503, 23.00000000000000000 ) ) ;
#9252=ORIENTED_EDGE ( 'NONE', *, *, #10202, .F. ) ;
#9260=AXIS2_PLACEMENT_3D ( 'NONE', #12929, #11893, #3381 ) ;
#9265=ORIENTED_EDGE ( 'NONE', *, *, #9178, .T. ) ;
#9276=DIRECTION ( 'NONE',  ( 0.000000000000000000, 1.000000000000000000, -0.000000000000000000 ) ) ;
#9281=ORIENTED_EDGE ( 'NONE', *, *, #13449, .T. ) ;
#9286=EDGE_LOOP ( 'NONE', ( #7398, #9063 ) ) ;
#9289=VECTOR ( 'NONE', #2119, 1000.000000000000000 ) ;
#9291=DIRECTION ( 'NONE',  ( 1.000000000000000000, 0.000000000000000000, 0.000000000000000000 ) ) ;
#9292=LINE ( 'NONE', #13540, #6421 ) ;
#9296=AXIS2_PLACEMENT_3D ( 'NONE', #1044, #6940, #4077 ) ;
#9298=ADVANCED_FACE ( 'NONE', ( #190 ), #4463, .T. ) ;
#9306=ORIENTED_EDGE ( 'NONE', *, *, #9034, .T. ) ;
#9310=DIRECTION ( 'NONE',  ( 0.7071067811865451302, -0.7071067811865500152, -0.000000000000000000 ) ) ;
#9313=CARTESIAN_POINT ( 'NONE',  ( 50.63563590245420443, 108.9054980190242503, 22.75000000000000000 ) ) ;
#9315=ORIENTED_EDGE ( 'NONE', *, *, #8395, .F. ) ;
#9319=EDGE_CURVE ( 'NONE', #10483, #5517, #11761, .T. ) ;
#9326=FACE_BOUND ( 'NONE', #1194, .T. ) ;
#9341=DIRECTION ( 'NONE',  ( 1.000000000000000000, 0.000000000000000000, 0.000000000000000000 ) ) ;
#9355=DIRECTION ( 'NONE',  ( 0.7071067811865451302, -0.7071067811865500152, -0.000000000000000000 ) ) ;
#9357=ORIENTED_EDGE ( 'NONE', *, *, #1447, .T. ) ;
#9359=LINE ( 'NONE', #10339, #1343 ) ;
#9361=CARTESIAN_POINT ( 'NONE',  ( 42.63563590245419732, 111.0390816101113387, 20.00000000000000000 ) ) ;
#9389=ORIENTED_EDGE ( 'NONE', *, *, #12363, .F. ) ;
#9394=ORIENTED_EDGE ( 'NONE', *, *, #1257, .F. ) ;
#9403=EDGE_CURVE ( 'NONE', #6080, #5517, #2527, .T. ) ;
#9404=CARTESIAN_POINT ( 'NONE',  ( 76.11748380738829667, 82.61803701715820125, 19.25000000000000000 ) ) ;
#9422=FACE_OUTER_BOUND ( 'NONE', #11659, .T. ) ;
#9424=CARTESIAN_POINT ( 'NONE',  ( 140.6356359024541973, 89.90549801902423610, 20.00000000000000000 ) ) ;
#9427=EDGE_LOOP ( 'NONE', ( #2362, #8413, #6046, #6428 ) ) ;
#9431=CARTESIAN_POINT ( 'NONE',  ( 140.6356359024541973, 113.0390816101113387, 19.25000000000000000 ) ) ;
#9432=ADVANCED_FACE ( 'NONE', ( #3487 ), #8926, .T. ) ;
#9439=CYLINDRICAL_SURFACE ( 'NONE', #4864, 0.2500000000000002220 ) ;
#9442=ORIENTED_EDGE ( 'NONE', *, *, #12030, .T. ) ;
#9443=ORIENTED_EDGE ( 'NONE', *, *, #6358, .T. ) ;
#9444=EDGE_CURVE ( 'NONE', #8730, #4150, #3961, .T. ) ;
#9447=CARTESIAN_POINT ( 'NONE',  ( 140.6356359024541973, 89.90549801902423610, 22.75000000000000000 ) ) ;
#9449=EDGE_CURVE ( 'NONE', #3613, #7821, #1872, .T. ) ;
#9450=CARTESIAN_POINT ( 'NONE',  ( 140.6356359024541973, 108.9054980190242503, 23.00000000000000000 ) ) ;
#9461=EDGE_LOOP ( 'NONE', ( #6847, #8058, #3052, #7664 ) ) ;
#9464=CARTESIAN_POINT ( 'NONE',  ( 112.1804561881462945, 85.03908161011133870, 0.7500000000000006661 ) ) ;
#9470=DIRECTION ( 'NONE',  ( -1.000000000000000000, 0.000000000000000000, 0.000000000000000000 ) ) ;
#9473=ORIENTED_EDGE ( 'NONE', *, *, #7998, .T. ) ;
#9485=EDGE_CURVE ( 'NONE', #8835, #12176, #881, .T. ) ;
#9486=CARTESIAN_POINT ( 'NONE',  ( 140.6356359024541973, 89.90549801902423610, 22.75000000000000000 ) ) ;
#9490=DIRECTION ( 'NONE',  ( -0.000000000000000000, -1.000000000000000000, 0.000000000000000000 ) ) ;
#9491=VERTEX_POINT ( 'NONE', #958 ) ;
#9494=CARTESIAN_POINT ( 'NONE',  ( 116.7775623211734342, 85.78908161011133870, 0.7500000000000000000 ) ) ;
#9500=VECTOR ( 'NONE', #3828, 1000.000000000000000 ) ;
#9503=ORIENTED_EDGE ( 'NONE', *, *, #4447, .T. ) ;
#9504=ORIENTED_EDGE ( 'NONE', *, *, #3739, .T. ) ;
#9506=CARTESIAN_POINT ( 'NONE',  ( 50.63563590245420443, 89.90549801902423610, 22.75000000000000000 ) ) ;
#9508=FACE_OUTER_BOUND ( 'NONE', #11689, .T. ) ;
#9512=VECTOR ( 'NONE', #11677, 999.9999999999998863 ) ;
#9517=VERTEX_POINT ( 'NONE', #2800 ) ;
#9518=( BOUNDED_CURVE ( )  B_SPLINE_CURVE ( 3, ( #6907, #8950, #2815, #13205 ),
 .UNSPECIFIED., .F., .F. ) 
 B_SPLINE_CURVE_WITH_KNOTS ( ( 4, 4 ),
 ( 4.712388980384689674, 6.283185307179586232 ),
 .UNSPECIFIED. ) 
 CURVE ( )  GEOMETRIC_REPRESENTATION_ITEM ( )  RATIONAL_B_SPLINE_CURVE ( ( 1.000000000000000000, 0.8047378541243649375, 0.8047378541243649375, 1.000000000000000000 ) ) 
 REPRESENTATION_ITEM ( '' )  );
#9520=ORIENTED_EDGE ( 'NONE', *, *, #12696, .F. ) ;
#9521=ORIENTED_EDGE ( 'NONE', *, *, #11013, .T. ) ;
#9522=DIRECTION ( 'NONE',  ( 1.000000000000000000, -0.000000000000000000, -0.000000000000000000 ) ) ;
#9523=CARTESIAN_POINT ( 'NONE',  ( 42.94629607423402007, 87.16776126655173584, 20.00000000000000000 ) ) ;
#9528=CARTESIAN_POINT ( 'NONE',  ( 116.7775623211734342, 75.03908161011133870, 20.00000000000000000 ) ) ;
#9531=EDGE_CURVE ( 'NONE', #1997, #4071, #5068, .T. ) ;
#9537=ORIENTED_EDGE ( 'NONE', *, *, #5245, .F. ) ;
#9539=CARTESIAN_POINT ( 'NONE',  ( 50.38563590245420443, 90.15549801902423610, 23.00000000000000000 ) ) ;
#9542=CARTESIAN_POINT ( 'NONE',  ( 50.38563590245420443, 108.6554980190242503, 23.00000000000000000 ) ) ;
#9547=CARTESIAN_POINT ( 'NONE',  ( 142.6356359024541973, 87.03908161011133870, 19.68933982822018081 ) ) ;
#9566=VECTOR ( 'NONE', #1593, 1000.000000000000000 ) ;
#9576=CARTESIAN_POINT ( 'NONE',  ( 141.8856359024541973, 110.7284214383315089, 20.00000000000000000 ) ) ;
#9580=LINE ( 'NONE', #12661, #7805 ) ;
#9584=VERTEX_POINT ( 'NONE', #11647 ) ;
#9587=VERTEX_POINT ( 'NONE', #4314 ) ;
#9590=AXIS2_PLACEMENT_3D ( 'NONE', #7769, #8823, #240 ) ;
#9591=ADVANCED_FACE ( 'NONE', ( #2369 ), #6464, .T. ) ;
#9596=ORIENTED_EDGE ( 'NONE', *, *, #9124, .F. ) ;
#9602=FACE_OUTER_BOUND ( 'NONE', #895, .T. ) ;
#9604=ORIENTED_EDGE ( 'NONE', *, *, #8769, .F. ) ;
#9607=VECTOR ( 'NONE', #9310, 1000.000000000000114 ) ;
#9612=EDGE_CURVE ( 'NONE', #5932, #13749, #1779, .T. ) ;
#9613=( LENGTH_UNIT ( ) NAMED_UNIT ( * ) SI_UNIT ( .MILLI., .METRE. ) );
#9626=CARTESIAN_POINT ( 'NONE',  ( 111.0903281124166710, 100.8715034839261762, 20.00000000000000000 ) ) ;
#9628=ADVANCED_FACE ( 'NONE', ( #5409 ), #6595, .T. ) ;
#9635=MANIFOLD_SOLID_BREP ( 'Mirror1', #8371 ) ;
#9639=DIRECTION ( 'NONE',  ( 1.000000000000000000, 0.000000000000000000, -0.000000000000000000 ) ) ;
#9642=AXIS2_PLACEMENT_3D ( 'NONE', #1450, #10976, #6616 ) ;
#9652=CARTESIAN_POINT ( 'NONE',  ( 76.18094369249178044, 97.20665973629650125, 10.00000000000000000 ) ) ;
#9656=FACE_OUTER_BOUND ( 'NONE', #304, .T. ) ;
#9665=VERTEX_POINT ( 'NONE', #8555 ) ;
#9669=CARTESIAN_POINT ( 'NONE',  ( 0.000000000000000000, 108.6554980190242503, 22.75000000000000000 ) ) ;
#9671=EDGE_LOOP ( 'NONE', ( #7373, #9252, #987, #5433 ) ) ;
#9674=DIRECTION ( 'NONE',  ( 1.000000000000000000, 0.000000000000000000, 0.000000000000000000 ) ) ;
#9690=CARTESIAN_POINT ( 'NONE',  ( 142.3249757306743675, 87.16776126655166479, 20.00000000000000000 ) ) ;
#9693=( BOUNDED_CURVE ( )  B_SPLINE_CURVE ( 3, ( #2541, #8865, #4812, #13259 ),
 .UNSPECIFIED., .F., .F. ) 
 B_SPLINE_CURVE_WITH_KNOTS ( ( 4, 4 ),
 ( 3.141592653589792672, 4.712388980384689674 ),
 .UNSPECIFIED. ) 
 CURVE ( )  GEOMETRIC_REPRESENTATION_ITEM ( )  RATIONAL_B_SPLINE_CURVE ( ( 1.000000000000000000, 0.8047378541243649375, 0.8047378541243649375, 1.000000000000000000 ) ) 
 REPRESENTATION_ITEM ( '' )  );
#9694=EDGE_CURVE ( 'NONE', #878, #12860, #5955, .T. ) ;
#9710=VERTEX_POINT ( 'NONE', #9898 ) ;
#9721=FACE_OUTER_BOUND ( 'NONE', #12601, .T. ) ;
#9726=ORIENTED_EDGE ( 'NONE', *, *, #7067, .F. ) ;
#9727=ORIENTED_EDGE ( 'NONE', *, *, #13635, .T. ) ;
#9729=ADVANCED_FACE ( 'NONE', ( #11141 ), #9040, .T. ) ;
#9730=DIRECTION ( 'NONE',  ( -0.000000000000000000, -0.000000000000000000, -1.000000000000000000 ) ) ;
#9741=EDGE_LOOP ( 'NONE', ( #13656, #267, #10635, #2489 ) ) ;
#9742=EDGE_CURVE ( 'NONE', #10095, #8747, #323, .T. ) ;
#9744=CARTESIAN_POINT ( 'NONE',  ( 84.99521369064696330, 82.14063840035363739, 10.00000000000000000 ) ) ;
#9745=CARTESIAN_POINT ( 'NONE',  ( 68.49370948373500312, 85.78908161011133870, 19.25000000000000000 ) ) ;
#9746=SURFACE_STYLE_FILL_AREA ( #8489 ) ;
#9749=DIRECTION ( 'NONE',  ( 0.000000000000000000, 0.000000000000000000, 1.000000000000000000 ) ) ;
#9761=ORIENTED_EDGE ( 'NONE', *, *, #12850, .F. ) ;
#9763=EDGE_LOOP ( 'NONE', ( #9473, #7673, #3020, #5480 ) ) ;
#9770=EDGE_LOOP ( 'NONE', ( #1766, #8100, #1208, #1059 ) ) ;
#9774=LINE ( 'NONE', #10894, #8779 ) ;
#9778=VECTOR ( 'NONE', #309, 1000.000000000000000 ) ;
#9783=VECTOR ( 'NONE', #12996, 1000.000000000000000 ) ;
#9788=PLANE ( 'NONE',  #8939 ) ;
#9808=DIRECTION ( 'NONE',  ( 1.000000000000000000, 0.000000000000000000, 0.000000000000000000 ) ) ;
#9828=ORIENTED_EDGE ( 'NONE', *, *, #1777, .F. ) ;
#9829=DIRECTION ( 'NONE',  ( -1.000000000000000000, 0.000000000000000000, 0.000000000000000000 ) ) ;
#9831=EDGE_CURVE ( 'NONE', #6295, #9665, #5508, .T. ) ;
#9834=EDGE_LOOP ( 'NONE', ( #1416, #10274, #4354, #3601 ) ) ;
#9840=( NAMED_UNIT ( * ) PLANE_ANGLE_UNIT ( ) SI_UNIT ( $, .RADIAN. ) );
#9853=LINE ( 'NONE', #10887, #4471 ) ;
#9860=CARTESIAN_POINT ( 'NONE',  ( 42.63563590245419732, 87.03908161011136713, 0.7500000000000006661 ) ) ;
#9861=DIRECTION ( 'NONE',  ( 0.000000000000000000, 0.000000000000000000, 1.000000000000000000 ) ) ;
#9872=FACE_OUTER_BOUND ( 'NONE', #8941, .T. ) ;
#9877=EDGE_CURVE ( 'NONE', #12198, #6660, #2849, .T. ) ;
#9881=ORIENTED_EDGE ( 'NONE', *, *, #3685, .T. ) ;
#9896=DIRECTION ( 'NONE',  ( 0.000000000000000000, 0.000000000000000000, 1.000000000000000000 ) ) ;
#9898=CARTESIAN_POINT ( 'NONE',  ( 140.6356359024541973, 108.9054980190242503, 20.00000000000000000 ) ) ;
#9903=CARTESIAN_POINT ( 'NONE',  ( 100.2760581142613603, 115.9375248198690826, 10.00000000000000000 ) ) ;
#9904=PLANE ( 'NONE',  #12027 ) ;
#9906=AXIS2_PLACEMENT_3D ( 'NONE', #9177, #12450, #5939 ) ;
#9913=CARTESIAN_POINT ( 'NONE',  ( 92.63563590245421153, 99.03908161011133870, 19.25000000000000000 ) ) ;
#9925=CARTESIAN_POINT ( 'NONE',  ( 134.6356359024541973, 108.9054980190242503, 23.00000000000000000 ) ) ;
#9943=ORIENTED_EDGE ( 'NONE', *, *, #12666, .T. ) ;
#9948=ADVANCED_FACE ( 'NONE', ( #11419, #3947 ), #8195, .F. ) ;
#9952=AXIS2_PLACEMENT_3D ( 'NONE', #802, #4106, #12406 ) ;
#9960=CARTESIAN_POINT ( 'NONE',  ( 103.4499059006094512, 83.97306027416853169, 10.00000000000000000 ) ) ;
#9968=EDGE_CURVE ( 'NONE', #11622, #7715, #871, .T. ) ;
#9970=VERTEX_POINT ( 'NONE', #1062 ) ;
#9972=( BOUNDED_CURVE ( )  B_SPLINE_CURVE ( 3, ( #3066, #7278, #11568, #7350 ),
 .UNSPECIFIED., .F., .F. ) 
 B_SPLINE_CURVE_WITH_KNOTS ( ( 4, 4 ),
 ( 3.141592653589793116, 4.712388980384689674 ),
 .UNSPECIFIED. ) 
 CURVE ( )  GEOMETRIC_REPRESENTATION_ITEM ( )  RATIONAL_B_SPLINE_CURVE ( ( 1.000000000000000000, 0.8047378541243649375, 0.8047378541243649375, 1.000000000000000000 ) ) 
 REPRESENTATION_ITEM ( '' )  );
#9983=DIRECTION ( 'NONE',  ( 0.000000000000000000, 1.000000000000000000, 0.000000000000000000 ) ) ;
#9984=EDGE_CURVE ( 'NONE', #9584, #3775, #5320, .T. ) ;
#9992=VERTEX_POINT ( 'NONE', #8605 ) ;
#9994=DIRECTION ( 'NONE',  ( -1.000000000000000000, 0.000000000000000000, 0.000000000000000000 ) ) ;
#10001=LINE ( 'NONE', #2476, #7793 ) ;
#10002=CARTESIAN_POINT ( 'NONE',  ( 134.6356359024541973, 108.9054980190242503, 20.00000000000000000 ) ) ;
#10003=ADVANCED_FACE ( 'NONE', ( #7460 ), #5390, .T. ) ;
#10004=ORIENTED_EDGE ( 'NONE', *, *, #7266, .F. ) ;
#10013=LINE ( 'NONE', #438, #6652 ) ;
#10015=EDGE_LOOP ( 'NONE', ( #11898, #5131, #3865, #11707 ) ) ;
#10030=ADVANCED_FACE ( 'NONE', ( #3388 ), #941, .F. ) ;
#10032=DIRECTION ( 'NONE',  ( 0.000000000000000000, -0.000000000000000000, 1.000000000000000000 ) ) ;
#10034=ORIENTED_EDGE ( 'NONE', *, *, #8687, .F. ) ;
#10044=AXIS2_PLACEMENT_3D ( 'NONE', #1024, #47, #5215 ) ;
#10049=CARTESIAN_POINT ( 'NONE',  ( 42.63563590245419732, 111.0390816101113387, 19.25000000000000000 ) ) ;
#10050=ORIENTED_EDGE ( 'NONE', *, *, #9319, .F. ) ;
#10051=CARTESIAN_POINT ( 'NONE',  ( 44.63563590245421864, 85.03908161011133870, 19.25000000000000000 ) ) ;
#10054=CYLINDRICAL_SURFACE ( 'NONE', #2057, 0.7500000000000072164 ) ;
#10055=VECTOR ( 'NONE', #11115, 999.9999999999998863 ) ;
#10062=FACE_OUTER_BOUND ( 'NONE', #187, .T. ) ;
#10069=ORIENTED_EDGE ( 'NONE', *, *, #11732, .F. ) ;
#10077=AXIS2_PLACEMENT_3D ( 'NONE', #12881, #5469, #3330 ) ;
#10080=CIRCLE ( 'NONE', #10293, 0.7499999999999966693 ) ;
#10084=EDGE_CURVE ( 'NONE', #3512, #11310, #2137, .T. ) ;
#10095=VERTEX_POINT ( 'NONE', #7337 ) ;
#10100=CARTESIAN_POINT ( 'NONE',  ( 123.1053058165639555, 68.56941169600116837, 0.7500000000000000000 ) ) ;
#10104=CARTESIAN_POINT ( 'NONE',  ( 44.73918929304747394, 108.8019446284309737, 23.00000000000000000 ) ) ;
#10105=ORIENTED_EDGE ( 'NONE', *, *, #4968, .F. ) ;
#10111=DIRECTION ( 'NONE',  ( 0.000000000000000000, 0.000000000000000000, 1.000000000000000000 ) ) ;
#10122=DIRECTION ( 'NONE',  ( 1.000000000000000000, -0.000000000000000000, -0.000000000000000000 ) ) ;
#10123=CARTESIAN_POINT ( 'NONE',  ( 44.63563590245423285, 113.0390816101113387, 19.68933982822018081 ) ) ;
#10124=DIRECTION ( 'NONE',  ( 0.000000000000000000, 0.000000000000000000, -1.000000000000000000 ) ) ;
#10125=VECTOR ( 'NONE', #6792, 1000.000000000000000 ) ;
#10129=DIRECTION ( 'NONE',  ( 1.000000000000000000, -0.000000000000000000, -0.000000000000000000 ) ) ;
#10138=CARTESIAN_POINT ( 'NONE',  ( 68.49370948373500312, 112.2890816101113387, 0.7500000000000006661 ) ) ;
#10140=ORIENTED_EDGE ( 'NONE', *, *, #5166, .T. ) ;
#10152=ORIENTED_EDGE ( 'NONE', *, *, #9449, .T. ) ;
#10158=PLANE ( 'NONE',  #8068 ) ;
#10168=ORIENTED_EDGE ( 'NONE', *, *, #12767, .T. ) ;
#10174=DIRECTION ( 'NONE',  ( -1.000000000000000000, 0.000000000000000000, 0.000000000000000000 ) ) ;
#10181=EDGE_CURVE ( 'NONE', #9710, #7171, #5664, .T. ) ;
#10182=ORIENTED_EDGE ( 'NONE', *, *, #10802, .F. ) ;
#10185=ORIENTED_EDGE ( 'NONE', *, *, #447, .T. ) ;
#10187=CARTESIAN_POINT ( 'NONE',  ( 44.63563590245422574, 113.0390816101113387, 20.00000000000000000 ) ) ;
#10195=CARTESIAN_POINT ( 'NONE',  ( 100.2760581142613603, 115.9375248198690826, 10.00000000000000000 ) ) ;
#10196=LINE ( 'NONE', #612, #10461 ) ;
#10198=VERTEX_POINT ( 'NONE', #9028 ) ;
#10199=AXIS2_PLACEMENT_3D ( 'NONE', #9152, #3648, #12159 ) ;
#10202=EDGE_CURVE ( 'NONE', #3775, #4364, #13224, .T. ) ;
#10205=DIRECTION ( 'NONE',  ( -0.000000000000000000, -0.000000000000000000, -1.000000000000000000 ) ) ;
#10208=CARTESIAN_POINT ( 'NONE',  ( 92.63563590245421153, 99.03908161011133870, 20.00000000000000000 ) ) ;
#10224=EDGE_CURVE ( 'NONE', #11751, #3428, #6853, .T. ) ;
#10244=EDGE_LOOP ( 'NONE', ( #5043, #6497, #12405, #437 ) ) ;
#10250=ORIENTED_EDGE ( 'NONE', *, *, #8798, .T. ) ;
#10257=ORIENTED_EDGE ( 'NONE', *, *, #10266, .T. ) ;
#10259=CARTESIAN_POINT ( 'NONE',  ( 43.38563590245419732, 99.03908161011133870, 0.000000000000000000 ) ) ;
#10261=DIRECTION ( 'NONE',  ( 1.000000000000000000, -0.000000000000000000, -0.000000000000000000 ) ) ;
#10263=CARTESIAN_POINT ( 'NONE',  ( 134.6356359024541973, 94.90549801902425031, 23.00000000000000000 ) ) ;
#10265=LINE ( 'NONE', #7871, #6493 ) ;
#10266=EDGE_CURVE ( 'NONE', #13640, #2183, #12820, .T. ) ;
#10274=ORIENTED_EDGE ( 'NONE', *, *, #10084, .F. ) ;
#10278=CARTESIAN_POINT ( 'NONE',  ( 116.7775623211734342, 112.2890816101113387, 19.25000000000000000 ) ) ;
#10285=ADVANCED_FACE ( 'NONE', ( #4006 ), #2701, .F. ) ;
#10286=EDGE_LOOP ( 'NONE', ( #13672, #8372, #8246, #12863 ) ) ;
#10289=ORIENTED_EDGE ( 'NONE', *, *, #447, .F. ) ;
#10290=AXIS2_PLACEMENT_3D ( 'NONE', #72, #3367, #13753 ) ;
#10291=CARTESIAN_POINT ( 'NONE',  ( 83.82136590429891498, 114.1051029460540605, 20.00000000000000000 ) ) ;
#10293=AXIS2_PLACEMENT_3D ( 'NONE', #4177, #10387, #2945 ) ;
#10297=CARTESIAN_POINT ( 'NONE',  ( 134.6356359024541973, 108.9054980190242503, 22.75000000000000000 ) ) ;
#10300=DIRECTION ( 'NONE',  ( 0.000000000000000000, -0.000000000000000000, -1.000000000000000000 ) ) ;
#10306=DIRECTION ( 'NONE',  ( 1.000000000000000000, 0.000000000000000000, -0.000000000000000000 ) ) ;
#10309=CARTESIAN_POINT ( 'NONE',  ( 116.7775623211734342, 75.03908161011133870, 20.00000000000000000 ) ) ;
#10311=FACE_BOUND ( 'NONE', #7733, .T. ) ;
#10313=ORIENTED_EDGE ( 'NONE', *, *, #7820, .F. ) ;
#10316=CIRCLE ( 'NONE', #12550, 2.000000000000001776 ) ;
#10318=DIRECTION ( 'NONE',  ( 0.000000000000000000, 0.000000000000000000, 1.000000000000000000 ) ) ;
#10319=EDGE_LOOP ( 'NONE', ( #392, #10443, #13675, #11269 ) ) ;
#10320=ORIENTED_EDGE ( 'NONE', *, *, #2752, .F. ) ;
#10323=LINE ( 'NONE', #5209, #3829 ) ;
#10329=CARTESIAN_POINT ( 'NONE',  ( 50.53208251186094202, 94.80194462843097369, 23.00000000000000000 ) ) ;
#10339=CARTESIAN_POINT ( 'NONE',  ( 45.16596598834414777, 112.5087515242214238, 0.000000000000000000 ) ) ;
#10341=( BOUNDED_CURVE ( )  B_SPLINE_CURVE ( 3, ( #10404, #12644, #980, #7111 ),
 .UNSPECIFIED., .F., .F. ) 
 B_SPLINE_CURVE_WITH_KNOTS ( ( 4, 4 ),
 ( 0.000000000000000000, 1.570796326794896558 ),
 .UNSPECIFIED. ) 
 CURVE ( )  GEOMETRIC_REPRESENTATION_ITEM ( )  RATIONAL_B_SPLINE_CURVE ( ( 1.000000000000000000, 0.8047378541243649375, 0.8047378541243649375, 1.000000000000000000 ) ) 
 REPRESENTATION_ITEM ( '' )  );
#10343=CYLINDRICAL_SURFACE ( 'NONE', #8929, 0.2500000000000002220 ) ;
#10345=ORIENTED_EDGE ( 'NONE', *, *, #11008, .F. ) ;
#10346=EDGE_CURVE ( 'NONE', #6180, #3595, #13557, .T. ) ;
#10354=CARTESIAN_POINT ( 'NONE',  ( 142.6356359024541973, 87.03908161011133870, 0.7500000000000006661 ) ) ;
#10359=ORIENTED_EDGE ( 'NONE', *, *, #12832, .F. ) ;
#10366=EDGE_LOOP ( 'NONE', ( #6937, #11123, #20, #1901 ) ) ;
#10370=DIRECTION ( 'NONE',  ( 1.000000000000000000, 0.000000000000000000, 0.000000000000000000 ) ) ;
#10387=DIRECTION ( 'NONE',  ( -0.7050191076322684935, -0.7091883091770476710, 0.000000000000000000 ) ) ;
#10391=ORIENTED_EDGE ( 'NONE', *, *, #8063, .T. ) ;
#10392=CIRCLE ( 'NONE', #1239, 0.7499999999999966693 ) ;
#10393=ORIENTED_EDGE ( 'NONE', *, *, #8156, .F. ) ;
#10395=LINE ( 'NONE', #12493, #1684 ) ;
#10404=CARTESIAN_POINT ( 'NONE',  ( 134.6356359024541973, 94.90549801902425031, 22.75000000000000000 ) ) ;
#10406=ADVANCED_FACE ( 'NONE', ( #11681 ), #11535, .T. ) ;
#10412=DIRECTION ( 'NONE',  ( 1.000000000000000000, -0.000000000000000000, 0.000000000000000000 ) ) ;
#10420=CYLINDRICAL_SURFACE ( 'NONE', #7577, 0.7499999999999973355 ) ;
#10432=CARTESIAN_POINT ( 'NONE',  ( 92.63563590245421153, 99.03908161011133870, 0.000000000000000000 ) ) ;
#10436=AXIS2_PLACEMENT_3D ( 'NONE', #12036, #7613, #1132 ) ;
#10442=EDGE_LOOP ( 'NONE', ( #1129, #4371, #12350, #11327 ) ) ;
#10443=ORIENTED_EDGE ( 'NONE', *, *, #7067, .T. ) ;
#10444=EDGE_CURVE ( 'NONE', #12702, #12568, #1188, .T. ) ;
#10445=AXIS2_PLACEMENT_3D ( 'NONE', #5493, #5362, #6557 ) ;
#10446=CIRCLE ( 'NONE', #2893, 9.999999999999994671 ) ;
#10452=CARTESIAN_POINT ( 'NONE',  ( 103.4499059006094512, 83.97306027416853169, 10.00000000000000000 ) ) ;
#10461=VECTOR ( 'NONE', #4683, 1000.000000000000000 ) ;
#10463=VECTOR ( 'NONE', #7254, 1000.000000000000000 ) ;
#10474=CARTESIAN_POINT ( 'NONE',  ( 134.8856359024541973, 94.65549801902425031, 23.00000000000000000 ) ) ;
#10476=DIRECTION ( 'NONE',  ( -0.000000000000000000, 1.000000000000000000, -0.000000000000000000 ) ) ;
#10480=AXIS2_PLACEMENT_3D ( 'NONE', #11386, #8243, #13415 ) ;
#10483=VERTEX_POINT ( 'NONE', #3040 ) ;
#10486=EDGE_CURVE ( 'NONE', #11310, #9517, #3241, .T. ) ;
#10487=CARTESIAN_POINT ( 'NONE',  ( 140.6356359024541973, 89.90549801902423610, 22.89644660940672694 ) ) ;
#10488=FACE_OUTER_BOUND ( 'NONE', #1409, .T. ) ;
#10498=DIRECTION ( 'NONE',  ( 0.000000000000000000, 1.000000000000000000, -0.000000000000000000 ) ) ;
#10504=CIRCLE ( 'NONE', #4482, 2.000000000000001776 ) ;
#10514=PLANE ( 'NONE',  #11005 ) ;
#10517=PLANE ( 'NONE',  #6689 ) ;
#10524=CYLINDRICAL_SURFACE ( 'NONE', #3277, 2.000000000000001776 ) ;
#10526=CARTESIAN_POINT ( 'NONE',  ( 50.38563590245420443, 94.65549801902425031, 23.00000000000000000 ) ) ;
#10541=ORIENTED_EDGE ( 'NONE', *, *, #9485, .F. ) ;
#10544=VERTEX_POINT ( 'NONE', #7520 ) ;
#10550=CARTESIAN_POINT ( 'NONE',  ( 134.6356359024541973, 108.9054980190242503, 22.89644660940672694 ) ) ;
#10576=EDGE_CURVE ( 'NONE', #2952, #9970, #6824, .T. ) ;
#10577=ORIENTED_EDGE ( 'NONE', *, *, #8612, .T. ) ;
#10580=DIRECTION ( 'NONE',  ( -1.000000000000000000, 0.000000000000000000, 0.000000000000000000 ) ) ;
#10583=CYLINDRICAL_SURFACE ( 'NONE', #7567, 9.999999999999994671 ) ;
#10587=CARTESIAN_POINT ( 'NONE',  ( 92.63563590245421153, 99.03908161011133870, 0.000000000000000000 ) ) ;
#10590=CARTESIAN_POINT ( 'NONE',  ( 44.94629607423404849, 85.78908161011133870, 0.000000000000000000 ) ) ;
#10594=CARTESIAN_POINT ( 'NONE',  ( 140.6356359024541973, 103.9054980190242361, 23.00000000000000000 ) ) ;
#10595=CARTESIAN_POINT ( 'NONE',  ( 142.6356359024541973, 87.03908161011133870, 0.7500000000000006661 ) ) ;
#10596=EDGE_LOOP ( 'NONE', ( #8551, #8599, #11915, #9357 ) ) ;
#10604=ORIENTED_EDGE ( 'NONE', *, *, #2363, .T. ) ;
#10605=VERTEX_POINT ( 'NONE', #11161 ) ;
#10606=ORIENTED_EDGE ( 'NONE', *, *, #1225, .T. ) ;
#10607=ORIENTED_EDGE ( 'NONE', *, *, #3803, .F. ) ;
#10615=EDGE_CURVE ( 'NONE', #821, #11588, #12919, .T. ) ;
#10620=VERTEX_POINT ( 'NONE', #12074 ) ;
#10624=FACE_OUTER_BOUND ( 'NONE', #6089, .T. ) ;
#10632=EDGE_CURVE ( 'NONE', #7171, #10095, #4804, .T. ) ;
#10635=ORIENTED_EDGE ( 'NONE', *, *, #12911, .T. ) ;
#10645=CYLINDRICAL_SURFACE ( 'NONE', #8197, 0.2500000000000002220 ) ;
#10655=VECTOR ( 'NONE', #10951, 1000.000000000000000 ) ;
#10660=DIRECTION ( 'NONE',  ( 1.000000000000000000, -0.000000000000000000, 0.000000000000000000 ) ) ;
#10667=CIRCLE ( 'NONE', #837, 2.000000000000001776 ) ;
#10671=ORIENTED_EDGE ( 'NONE', *, *, #8464, .T. ) ;
#10674=EDGE_LOOP ( 'NONE', ( #2563, #5423, #7231, #11690 ) ) ;
#10684=AXIS2_PLACEMENT_3D ( 'NONE', #1727, #678, #9341 ) ;
#10688=CIRCLE ( 'NONE', #11813, 2.000000000000001776 ) ;
#10693=VERTEX_POINT ( 'NONE', #9136 ) ;
#10697=DIRECTION ( 'NONE',  ( -0.7071067811865474617, -0.7071067811865474617, 0.000000000000000000 ) ) ;
#10700=EDGE_CURVE ( 'NONE', #4490, #13747, #405, .T. ) ;
#10709=VECTOR ( 'NONE', #1895, 1000.000000000000000 ) ;
#10711=EDGE_CURVE ( 'NONE', #12138, #10605, #11326, .T. ) ;
#10712=TOROIDAL_SURFACE ( 'NONE', #4253, 10.75000000000000000, 0.7500000000000000000 ) ;
#10714=CARTESIAN_POINT ( 'NONE',  ( 123.1053058165639555, 68.56941169600116837, 20.00000000000000000 ) ) ;
#10729=CARTESIAN_POINT ( 'NONE',  ( 141.8856359024541973, 85.03908161011133870, 0.7500000000000006661 ) ) ;
#10733=DIRECTION ( 'NONE',  ( 0.000000000000000000, 0.000000000000000000, -1.000000000000000000 ) ) ;
#10737=DIRECTION ( 'NONE',  ( -1.000000000000000000, 0.000000000000000000, -0.000000000000000000 ) ) ;
#10740=CARTESIAN_POINT ( 'NONE',  ( 92.63563590245421153, 99.03908161011133870, 19.25000000000000000 ) ) ;
#10741=SHAPE_REPRESENTATION_RELATIONSHIP ( 'NONE' , 'NONE' ,  #12309, #5398 ) ;
#10742=ADVANCED_FACE ( 'NONE', ( #2942 ), #7091, .F. ) ;
#10743=EDGE_CURVE ( 'NONE', #13747, #1567, #2691, .T. ) ;
#10744=EDGE_CURVE ( 'NONE', #3595, #182, #2329, .T. ) ;
#10746=AXIS2_PLACEMENT_3D ( 'NONE', #12268, #12194, #8838 ) ;
#10749=VERTEX_POINT ( 'NONE', #8218 ) ;
#10754=FACE_OUTER_BOUND ( 'NONE', #1356, .T. ) ;
#10765=ORIENTED_EDGE ( 'NONE', *, *, #4240, .T. ) ;
#10770=DIRECTION ( 'NONE',  ( 0.7071067811865567876, 0.7071067811865382469, 0.000000000000000000 ) ) ;
#10772=DIRECTION ( 'NONE',  ( -1.000000000000000000, 0.000000000000000000, 0.000000000000000000 ) ) ;
#10780=EDGE_LOOP ( 'NONE', ( #4529, #2980, #6754, #11000 ) ) ;
#10782=EDGE_LOOP ( 'NONE', ( #362, #8815, #8400, #1340 ) ) ;
#10785=CARTESIAN_POINT ( 'NONE',  ( 142.6356359024541973, 85.03908161011133870, 20.00000000000000000 ) ) ;
#10786=ORIENTED_EDGE ( 'NONE', *, *, #12832, .T. ) ;
#10789=CARTESIAN_POINT ( 'NONE',  ( 141.8856359024541973, 110.7284214383315089, 0.000000000000000000 ) ) ;
#10799=ADVANCED_FACE ( 'NONE', ( #9422 ), #3777, .T. ) ;
#10802=EDGE_CURVE ( 'NONE', #6080, #1109, #13668, .T. ) ;
#10804=CARTESIAN_POINT ( 'NONE',  ( 116.7775623211734342, 112.2890816101113387, 0.7500000000000006661 ) ) ;
#10809=CARTESIAN_POINT ( 'NONE',  ( 134.8856359024541973, 0.000000000000000000, 22.75000000000000000 ) ) ;
#10815=ORIENTED_EDGE ( 'NONE', *, *, #7031, .T. ) ;
#10816=CARTESIAN_POINT ( 'NONE',  ( 134.6356359024541973, 89.90549801902423610, 20.00000000000000000 ) ) ;
#10828=ADVANCED_FACE ( 'NONE', ( #12821 ), #3208, .F. ) ;
#10830=EDGE_LOOP ( 'NONE', ( #922, #3251, #2956, #5218 ) ) ;
#10836=CARTESIAN_POINT ( 'NONE',  ( 44.63563590245421864, 85.03908161011133870, 19.25000000000000000 ) ) ;
#10838=DIRECTION ( 'NONE',  ( 1.000000000000000000, 0.000000000000000000, 0.000000000000000000 ) ) ;
#10841=DIRECTION ( 'NONE',  ( 1.000000000000000000, 0.000000000000000000, 0.000000000000000000 ) ) ;
#10844=ORIENTED_EDGE ( 'NONE', *, *, #2635, .T. ) ;
#10848=CYLINDRICAL_SURFACE ( 'NONE', #9260, 0.7499999999999924505 ) ;
#10867=LINE ( 'NONE', #1568, #3065 ) ;
#10868=CARTESIAN_POINT ( 'NONE',  ( 62.16596598834446752, 129.5087515242215090, 20.00000000000000000 ) ) ;
#10872=DIRECTION ( 'NONE',  ( 1.000000000000000000, 0.000000000000000000, 0.000000000000000000 ) ) ;
#10883=ORIENTED_EDGE ( 'NONE', *, *, #11990, .T. ) ;
#10886=EDGE_LOOP ( 'NONE', ( #4228, #4474, #10359, #13617 ) ) ;
#10887=CARTESIAN_POINT ( 'NONE',  ( 79.82136590429890077, 114.1051029460540605, 10.00000000000000000 ) ) ;
#10889=DIRECTION ( 'NONE',  ( 0.000000000000000000, 0.000000000000000000, -1.000000000000000000 ) ) ;
#10890=CYLINDRICAL_SURFACE ( 'NONE', #242, 6.000000000000005329 ) ;
#10894=CARTESIAN_POINT ( 'NONE',  ( 142.6356359024541973, 111.0390816101113245, 20.00000000000000000 ) ) ;
#10896=VECTOR ( 'NONE', #3163, 1000.000000000000000 ) ;
#10897=AXIS2_PLACEMENT_3D ( 'NONE', #7993, #10111, #12266 ) ;
#10910=DIRECTION ( 'NONE',  ( 1.000000000000000000, 0.000000000000000000, -0.000000000000000000 ) ) ;
#10911=DIRECTION ( 'NONE',  ( 1.000000000000000000, -0.000000000000000000, 0.000000000000000000 ) ) ;
#10915=AXIS2_PLACEMENT_3D ( 'NONE', #3584, #4619, #8875 ) ;
#10924=VERTEX_POINT ( 'NONE', #6874 ) ;
#10926=LINE ( 'NONE', #3308, #4415 ) ;
#10930=CIRCLE ( 'NONE', #12487, 9.999999999999994671 ) ;
#10939=EDGE_CURVE ( 'NONE', #13640, #821, #4790, .T. ) ;
#10945=ORIENTED_EDGE ( 'NONE', *, *, #2809, .T. ) ;
#10946=DIRECTION ( 'NONE',  ( -0.000000000000000000, -0.000000000000000000, -1.000000000000000000 ) ) ;
#10951=DIRECTION ( 'NONE',  ( 0.000000000000000000, 0.000000000000000000, -1.000000000000000000 ) ) ;
#10952=LINE ( 'NONE', #1573, #11582 ) ;
#10957=AXIS2_PLACEMENT_3D ( 'NONE', #12368, #3916, #3649 ) ;
#10963=CIRCLE ( 'NONE', #10077, 2.000000000000001776 ) ;
#10970=EDGE_CURVE ( 'NONE', #6660, #2183, #13303, .T. ) ;
#10971=ORIENTED_EDGE ( 'NONE', *, *, #599, .F. ) ;
#10976=DIRECTION ( 'NONE',  ( -1.000000000000000000, 0.000000000000000000, 0.000000000000000000 ) ) ;
#10978=DIRECTION ( 'NONE',  ( -1.000000000000000000, -0.000000000000000000, -0.000000000000000000 ) ) ;
#10989=CARTESIAN_POINT ( 'NONE',  ( 134.6356359024541973, 103.9054980190242361, 22.75000000000000000 ) ) ;
#10995=ORIENTED_EDGE ( 'NONE', *, *, #4413, .T. ) ;
#10998=EDGE_CURVE ( 'NONE', #8025, #7886, #8379, .T. ) ;
#11000=ORIENTED_EDGE ( 'NONE', *, *, #12183, .F. ) ;
#11005=AXIS2_PLACEMENT_3D ( 'NONE', #4096, #2078, #8344 ) ;
#11008=EDGE_CURVE ( 'NONE', #7689, #1569, #13139, .T. ) ;
#11013=EDGE_CURVE ( 'NONE', #3980, #4904, #10667, .T. ) ;
#11030=CARTESIAN_POINT ( 'NONE',  ( 116.7775623211734342, 85.03908161011133870, 19.25000000000000000 ) ) ;
#11041=ORIENTED_EDGE ( 'NONE', *, *, #972, .F. ) ;
#11054=ORIENTED_EDGE ( 'NONE', *, *, #9984, .T. ) ;
#11058=ORIENTED_EDGE ( 'NONE', *, *, #12098, .F. ) ;
#11082=DIRECTION ( 'NONE',  ( -1.000000000000000000, 0.000000000000000000, 0.000000000000000000 ) ) ;
#11087=AXIS2_PLACEMENT_3D ( 'NONE', #8235, #3915, #2878 ) ;
#11089=VERTEX_POINT ( 'NONE', #6821 ) ;
#11092=DIRECTION ( 'NONE',  ( 0.000000000000000000, 0.000000000000000000, 1.000000000000000000 ) ) ;
#11095=PLANE ( 'NONE',  #6420 ) ;
#11098=DIRECTION ( 'NONE',  ( -0.000000000000000000, -1.000000000000000000, -0.000000000000000000 ) ) ;
#11105=EDGE_CURVE ( 'NONE', #13747, #7886, #7653, .T. ) ;
#11107=FACE_OUTER_BOUND ( 'NONE', #4093, .T. ) ;
#11110=FACE_OUTER_BOUND ( 'NONE', #4219, .T. ) ;
#11111=CARTESIAN_POINT ( 'NONE',  ( 44.63563590245420443, 94.90549801902425031, 23.00000000000000000 ) ) ;
#11115=DIRECTION ( 'NONE',  ( 0.7071067811865525687, 0.7071067811865425767, -0.000000000000000000 ) ) ;
#11118=ORIENTED_EDGE ( 'NONE', *, *, #6115, .T. ) ;
#11119=CIRCLE ( 'NONE', #12462, 0.7499999999999966693 ) ;
#11120=AXIS2_PLACEMENT_3D ( 'NONE', #885, #1943, #8219 ) ;
#11123=ORIENTED_EDGE ( 'NONE', *, *, #12942, .F. ) ;
#11140=EDGE_CURVE ( 'NONE', #10620, #11879, #6890, .T. ) ;
#11141=FACE_OUTER_BOUND ( 'NONE', #3519, .T. ) ;
#11146=CARTESIAN_POINT ( 'NONE',  ( 185.2712718049083946, 0.000000000000000000, 23.00000000000000000 ) ) ;
#11150=AXIS2_PLACEMENT_3D ( 'NONE', #389, #8780, #2377 ) ;
#11154=ADVANCED_FACE ( 'NONE', ( #2591 ), #11095, .F. ) ;
#11156=CARTESIAN_POINT ( 'NONE',  ( 140.6356359024541973, 113.0390816101113387, 20.00000000000000000 ) ) ;
#11161=CARTESIAN_POINT ( 'NONE',  ( 68.49370948373500312, 85.03908161011133870, 19.25000000000000000 ) ) ;
#11166=DIRECTION ( 'NONE',  ( 1.000000000000000000, 2.775557561562892929E-15, 0.000000000000000000 ) ) ;
#11168=VECTOR ( 'NONE', #8849, 1000.000000000000000 ) ;
#11170=VECTOR ( 'NONE', #2837, 1000.000000000000000 ) ;
#11176=ORIENTED_EDGE ( 'NONE', *, *, #468, .F. ) ;
#11183=DIRECTION ( 'NONE',  ( 0.7091883091770476710, -0.7050191076322684935, 0.000000000000000000 ) ) ;
#11188=ORIENTED_EDGE ( 'NONE', *, *, #468, .T. ) ;
#11200=DIRECTION ( 'NONE',  ( 0.000000000000000000, 0.000000000000000000, 1.000000000000000000 ) ) ;
#11211=EDGE_CURVE ( 'NONE', #5173, #12738, #412, .T. ) ;
#11212=ORIENTED_EDGE ( 'NONE', *, *, #7912, .F. ) ;
#11214=EDGE_LOOP ( 'NONE', ( #11800, #12120, #8257, #13074 ) ) ;
#11215=VECTOR ( 'NONE', #384, 1000.000000000000000 ) ;
#11226=EDGE_CURVE ( 'NONE', #8282, #12380, #5902, .T. ) ;
#11235=DIRECTION ( 'NONE',  ( 1.000000000000000000, 0.000000000000000000, 0.000000000000000000 ) ) ;
#11242=VECTOR ( 'NONE', #6149, 1000.000000000000000 ) ;
#11251=CARTESIAN_POINT ( 'NONE',  ( 134.8856359024541973, 104.1554980190242361, 23.00000000000000000 ) ) ;
#11256=CYLINDRICAL_SURFACE ( 'NONE', #3119, 24.04163056034261459 ) ;
#11259=DIRECTION ( 'NONE',  ( -1.000000000000000000, 0.000000000000000000, 0.000000000000000000 ) ) ;
#11260=ADVANCED_FACE ( 'NONE', ( #7267 ), #11341, .T. ) ;
#11262=ORIENTED_EDGE ( 'NONE', *, *, #7329, .T. ) ;
#11266=CARTESIAN_POINT ( 'NONE',  ( 44.63563590245420443, 89.90549801902423610, 22.75000000000000000 ) ) ;
#11269=ORIENTED_EDGE ( 'NONE', *, *, #9877, .T. ) ;
#11275=ORIENTED_EDGE ( 'NONE', *, *, #7150, .F. ) ;
#11276=ORIENTED_EDGE ( 'NONE', *, *, #3553, .F. ) ;
#11278=EDGE_LOOP ( 'NONE', ( #1603, #9727, #8636, #8588 ) ) ;
#11280=EDGE_LOOP ( 'NONE', ( #183, #269 ) ) ;
#11281=CARTESIAN_POINT ( 'NONE',  ( 111.0903281124166710, 100.8715034839261762, 10.00000000000000000 ) ) ;
#11295=DIRECTION ( 'NONE',  ( 0.000000000000000000, 0.000000000000000000, -1.000000000000000000 ) ) ;
#11298=EDGE_LOOP ( 'NONE', ( #10604, #12570, #11041, #3882 ) ) ;
#11306=DIRECTION ( 'NONE',  ( -0.000000000000000000, -0.000000000000000000, 1.000000000000000000 ) ) ;
#11310=VERTEX_POINT ( 'NONE', #5969 ) ;
#11315=CARTESIAN_POINT ( 'NONE',  ( 44.63563590245420443, 108.9054980190242503, 22.75000000000000000 ) ) ;
#11319=( BOUNDED_CURVE ( )  B_SPLINE_CURVE ( 3, ( #4186, #6344, #7650, #5220 ),
 .UNSPECIFIED., .F., .F. ) 
 B_SPLINE_CURVE_WITH_KNOTS ( ( 4, 4 ),
 ( 1.570796326794896558, 3.141592653589793116 ),
 .UNSPECIFIED. ) 
 CURVE ( )  GEOMETRIC_REPRESENTATION_ITEM ( )  RATIONAL_B_SPLINE_CURVE ( ( 1.000000000000000000, 0.8047378541243649375, 0.8047378541243649375, 1.000000000000000000 ) ) 
 REPRESENTATION_ITEM ( '' )  );
#11325=AXIS2_PLACEMENT_3D ( 'NONE', #12943, #561, #11183 ) ;
#11326=CIRCLE ( 'NONE', #1092, 9.999999999999994671 ) ;
#11327=ORIENTED_EDGE ( 'NONE', *, *, #6977, .F. ) ;
#11330=CARTESIAN_POINT ( 'NONE',  ( 109.6856792294029219, 115.9888905337886769, 19.25000000000000000 ) ) ;
#11333=CARTESIAN_POINT ( 'NONE',  ( 100.2760581142613603, 115.9375248198690826, 20.00000000000000000 ) ) ;
#11338=CARTESIAN_POINT ( 'NONE',  ( 68.49370948373500312, 123.0390816101113245, 0.7500000000000006661 ) ) ;
#11339=CARTESIAN_POINT ( 'NONE',  ( 98.27605811426136029, 115.9375248198690826, 10.00000000000000000 ) ) ;
#11341=TOROIDAL_SURFACE ( 'NONE', #11553, 10.75000000000000000, 0.7500000000000000000 ) ;
#11343=ADVANCED_FACE ( 'NONE', ( #13009 ), #3454, .F. ) ;
#11353=CARTESIAN_POINT ( 'NONE',  ( 74.18094369249178044, 97.20665973629650125, 10.00000000000000000 ) ) ;
#11354=DIRECTION ( 'NONE',  ( -1.000000000000000000, 0.000000000000000000, 0.000000000000000000 ) ) ;
#11359=ORIENTED_EDGE ( 'NONE', *, *, #9029, .T. ) ;
#11360=EDGE_CURVE ( 'NONE', #5517, #6706, #10926, .T. ) ;
#11361=AXIS2_PLACEMENT_3D ( 'NONE', #1187, #1328, #2122 ) ;
#11364=CARTESIAN_POINT ( 'NONE',  ( 50.53208251186094202, 90.00905140961751272, 23.00000000000000000 ) ) ;
#11369=CARTESIAN_POINT ( 'NONE',  ( 134.8856359024541973, 90.15549801902423610, 23.00000000000000000 ) ) ;
#11375=AXIS2_PLACEMENT_3D ( 'NONE', #108, #4382, #6400 ) ;
#11378=ORIENTED_EDGE ( 'NONE', *, *, #11585, .F. ) ;
#11382=CARTESIAN_POINT ( 'NONE',  ( 140.3856359024541973, 108.6554980190242503, 23.00000000000000000 ) ) ;
#11386=CARTESIAN_POINT ( 'NONE',  ( 134.6356359024541973, 108.9054980190242503, 23.00000000000000000 ) ) ;
#11392=EDGE_CURVE ( 'NONE', #9665, #6295, #3551, .T. ) ;
#11393=ORIENTED_EDGE ( 'NONE', *, *, #9968, .T. ) ;
#11395=ORIENTED_EDGE ( 'NONE', *, *, #7902, .F. ) ;
#11397=EDGE_LOOP ( 'NONE', ( #9107, #13070, #10883, #6143 ) ) ;
#11403=VECTOR ( 'NONE', #9118, 1000.000000000000000 ) ;
#11407=FACE_OUTER_BOUND ( 'NONE', #10015, .T. ) ;
#11412=AXIS2_PLACEMENT_3D ( 'NONE', #4098, #7149, #6164 ) ;
#11419=FACE_BOUND ( 'NONE', #8516, .T. ) ;
#11420=ADVANCED_FACE ( 'NONE', ( #7537 ), #231, .T. ) ;
#11425=CARTESIAN_POINT ( 'NONE',  ( 44.63563590245420443, 94.90549801902425031, 20.00000000000000000 ) ) ;
#11445=EDGE_CURVE ( 'NONE', #1998, #3512, #10446, .T. ) ;
#11459=CARTESIAN_POINT ( 'NONE',  ( 92.63563590245421153, 85.78908161011133870, 0.000000000000000000 ) ) ;
#11461=ORIENTED_EDGE ( 'NONE', *, *, #12687, .T. ) ;
#11467=VERTEX_POINT ( 'NONE', #11752 ) ;
#11472=LINE ( 'NONE', #7196, #11242 ) ;
#11495=CARTESIAN_POINT ( 'NONE',  ( 140.6356359024541973, 113.0390816101113387, 0.3106601717798218587 ) ) ;
#11500=CARTESIAN_POINT ( 'NONE',  ( 134.6356359024541973, 94.90549801902425031, 23.00000000000000000 ) ) ;
#11502=CARTESIAN_POINT ( 'NONE',  ( 134.6356359024541973, 89.90549801902423610, 22.75000000000000000 ) ) ;
#11518=DIRECTION ( 'NONE',  ( 0.000000000000000000, 0.000000000000000000, 1.000000000000000000 ) ) ;
#11528=ORIENTED_EDGE ( 'NONE', *, *, #12030, .F. ) ;
#11535=CYLINDRICAL_SURFACE ( 'NONE', #13573, 0.7499999999999973355 ) ;
#11541=AXIS2_PLACEMENT_3D ( 'NONE', #6381, #5394, #6321 ) ;
#11553=AXIS2_PLACEMENT_3D ( 'NONE', #2004, #940, #1723 ) ;
#11560=ADVANCED_FACE ( 'NONE', ( #12243 ), #2699, .T. ) ;
#11563=VECTOR ( 'NONE', #7601, 1000.000000000000000 ) ;
#11568=CARTESIAN_POINT ( 'NONE',  ( 140.5069562460138286, 112.7284214383315089, 20.00000000000000000 ) ) ;
#11571=ORIENTED_EDGE ( 'NONE', *, *, #2571, .F. ) ;
#11576=DIRECTION ( 'NONE',  ( 0.000000000000000000, 0.000000000000000000, 1.000000000000000000 ) ) ;
#11581=VECTOR ( 'NONE', #3295, 1000.000000000000000 ) ;
#11582=VECTOR ( 'NONE', #2375, 1000.000000000000000 ) ;
#11585=EDGE_CURVE ( 'NONE', #9992, #363, #10013, .T. ) ;
#11588=VERTEX_POINT ( 'NONE', #514 ) ;
#11590=EDGE_LOOP ( 'NONE', ( #8338, #7708, #6230, #3535 ) ) ;
#11595=DIRECTION ( 'NONE',  ( 1.000000000000000000, 0.000000000000000000, -0.000000000000000000 ) ) ;
#11606=FACE_OUTER_BOUND ( 'NONE', #12670, .T. ) ;
#11608=EDGE_CURVE ( 'NONE', #13266, #6817, #4215, .T. ) ;
#11614=CARTESIAN_POINT ( 'NONE',  ( 140.6356359024541973, 113.0390816101113387, 20.00000000000000000 ) ) ;
#11618=CIRCLE ( 'NONE', #13397, 0.7500000000000000000 ) ;
#11622=VERTEX_POINT ( 'NONE', #6010 ) ;
#11627=ADVANCED_FACE ( 'NONE', ( #11606 ), #7325, .F. ) ;
#11634=AXIS2_PLACEMENT_3D ( 'NONE', #8696, #12819, #10872 ) ;
#11636=AXIS2_PLACEMENT_3D ( 'NONE', #11146, #12056, #11082 ) ;
#11641=DIRECTION ( 'NONE',  ( -0.000000000000000000, -0.000000000000000000, 1.000000000000000000 ) ) ;
#11642=AXIS2_PLACEMENT_3D ( 'NONE', #6650, #13226, #2495 ) ;
#11647=CARTESIAN_POINT ( 'NONE',  ( 140.3249757306743675, 85.78908161011133870, 20.00000000000000000 ) ) ;
#11649=EDGE_CURVE ( 'NONE', #3543, #209, #11119, .T. ) ;
#11653=DIRECTION ( 'NONE',  ( 0.000000000000000000, -1.000000000000000000, 0.000000000000000000 ) ) ;
#11654=CARTESIAN_POINT ( 'NONE',  ( 0.000000000000000000, 0.000000000000000000, 0.000000000000000000 ) ) ;
#11659=EDGE_LOOP ( 'NONE', ( #4770, #12600, #11176, #10320 ) ) ;
#11661=ORIENTED_EDGE ( 'NONE', *, *, #2309, .T. ) ;
#11662=ORIENTED_EDGE ( 'NONE', *, *, #9984, .F. ) ;
#11665=ORIENTED_EDGE ( 'NONE', *, *, #7858, .F. ) ;
#11676=VERTEX_POINT ( 'NONE', #7191 ) ;
#11677=DIRECTION ( 'NONE',  ( 0.7071067811865525687, 0.7071067811865425767, -0.000000000000000000 ) ) ;
#11678=DIRECTION ( 'NONE',  ( -0.000000000000000000, -0.000000000000000000, -1.000000000000000000 ) ) ;
#11681=FACE_OUTER_BOUND ( 'NONE', #8885, .T. ) ;
#11689=EDGE_LOOP ( 'NONE', ( #935, #10289, #5521, #8824 ) ) ;
#11690=ORIENTED_EDGE ( 'NONE', *, *, #4768, .T. ) ;
#11692=ORIENTED_EDGE ( 'NONE', *, *, #4254, .T. ) ;
#11698=FACE_OUTER_BOUND ( 'NONE', #10442, .T. ) ;
#11707=ORIENTED_EDGE ( 'NONE', *, *, #10700, .F. ) ;
#11726=LINE ( 'NONE', #8441, #4884 ) ;
#11729=AXIS2_PLACEMENT_3D ( 'NONE', #12139, #1583, #13180 ) ;
#11732=EDGE_CURVE ( 'NONE', #6593, #6180, #292, .T. ) ;
#11738=CARTESIAN_POINT ( 'NONE',  ( 105.4499059006094654, 83.97306027416853169, 10.00000000000000000 ) ) ;
#11741=AXIS2_PLACEMENT_3D ( 'NONE', #11976, #5541, #10032 ) ;
#11744=ORIENTED_EDGE ( 'NONE', *, *, #9531, .F. ) ;
#11746=ORIENTED_EDGE ( 'NONE', *, *, #4162, .T. ) ;
#11751=VERTEX_POINT ( 'NONE', #11738 ) ;
#11752=CARTESIAN_POINT ( 'NONE',  ( 109.1537879975201406, 82.61803701715820125, 0.000000000000000000 ) ) ;
#11757=FACE_OUTER_BOUND ( 'NONE', #10830, .T. ) ;
#11758=CARTESIAN_POINT ( 'NONE',  ( 43.38563590245419732, 110.7284214383315089, 20.00000000000000000 ) ) ;
#11759=EDGE_CURVE ( 'NONE', #12630, #6080, #5507, .T. ) ;
#11761=( BOUNDED_CURVE ( )  B_SPLINE_CURVE ( 3, ( #478, #7864, #10123, #12279 ),
 .UNSPECIFIED., .F., .F. ) 
 B_SPLINE_CURVE_WITH_KNOTS ( ( 4, 4 ),
 ( 4.712388980384689674, 6.283185307179586232 ),
 .UNSPECIFIED. ) 
 CURVE ( )  GEOMETRIC_REPRESENTATION_ITEM ( )  RATIONAL_B_SPLINE_CURVE ( ( 1.000000000000000000, 0.8047378541243649375, 0.8047378541243649375, 1.000000000000000000 ) ) 
 REPRESENTATION_ITEM ( '' )  );
#11762=VERTEX_POINT ( 'NONE', #7392 ) ;
#11768=DIRECTION ( 'NONE',  ( 0.000000000000000000, 0.000000000000000000, 1.000000000000000000 ) ) ;
#11769=CARTESIAN_POINT ( 'NONE',  ( 50.63563590245420443, 108.9054980190242503, 22.89644660940672694 ) ) ;
#11774=CARTESIAN_POINT ( 'NONE',  ( 142.6356359024541973, 87.03908161011133870, 19.25000000000000000 ) ) ;
#11780=AXIS2_PLACEMENT_3D ( 'NONE', #4363, #12865, #3309 ) ;
#11784=ORIENTED_EDGE ( 'NONE', *, *, #3229, .F. ) ;
#11792=AXIS2_PLACEMENT_3D ( 'NONE', #1768, #2835, #12244 ) ;
#11793=ADVANCED_FACE ( 'NONE', ( #9872 ), #3442, .T. ) ;
#11795=FACE_OUTER_BOUND ( 'NONE', #8710, .T. ) ;
#11799=DIRECTION ( 'NONE',  ( -0.000000000000000000, -0.000000000000000000, 1.000000000000000000 ) ) ;
#11800=ORIENTED_EDGE ( 'NONE', *, *, #5164, .T. ) ;
#11805=CARTESIAN_POINT ( 'NONE',  ( 75.58559257550551536, 115.9888905337886769, 19.25000000000000000 ) ) ;
#11808=DIRECTION ( 'NONE',  ( -0.7071067811865451302, 0.7071067811865500152, 0.000000000000000000 ) ) ;
#11809=CARTESIAN_POINT ( 'NONE',  ( 123.1053058165644671, 129.5087515242213669, 19.25000000000000000 ) ) ;
#11810=CARTESIAN_POINT ( 'NONE',  ( 42.63563590245419732, 85.03908161011133870, 0.7500000000000006661 ) ) ;
#11813=AXIS2_PLACEMENT_3D ( 'NONE', #9626, #8429, #3144 ) ;
#11817=ADVANCED_FACE ( 'NONE', ( #7667 ), #8805, .T. ) ;
#11821=ORIENTED_EDGE ( 'NONE', *, *, #8798, .F. ) ;
#11822=VERTEX_POINT ( 'NONE', #211 ) ;
#11823=ORIENTED_EDGE ( 'NONE', *, *, #155, .F. ) ;
#11829=FACE_OUTER_BOUND ( 'NONE', #11278, .T. ) ;
#11831=CARTESIAN_POINT ( 'NONE',  ( 50.38563590245420443, 108.9054980190242503, 22.75000000000000000 ) ) ;
#11835=EDGE_CURVE ( 'NONE', #10693, #1263, #2676, .T. ) ;
#11842=EDGE_CURVE ( 'NONE', #7821, #13545, #5583, .T. ) ;
#11844=CARTESIAN_POINT ( 'NONE',  ( 84.99521369064696330, 82.14063840035363739, 10.00000000000000000 ) ) ;
#11847=VECTOR ( 'NONE', #8252, 1000.000000000000000 ) ;
#11851=DIRECTION ( 'NONE',  ( -1.000000000000000000, 0.000000000000000000, 0.000000000000000000 ) ) ;
#11853=FACE_OUTER_BOUND ( 'NONE', #5329, .T. ) ;
#11856=DIRECTION ( 'NONE',  ( 1.000000000000000000, 0.000000000000000000, 0.000000000000000000 ) ) ;
#11859=AXIS2_PLACEMENT_3D ( 'NONE', #8873, #12020, #3708 ) ;
#11878=EDGE_CURVE ( 'NONE', #209, #5173, #73, .T. ) ;
#11879=VERTEX_POINT ( 'NONE', #2267 ) ;
#11887=PLANE ( 'NONE',  #6903 ) ;
#11888=DIRECTION ( 'NONE',  ( -0.000000000000000000, -0.000000000000000000, -1.000000000000000000 ) ) ;
#11893=DIRECTION ( 'NONE',  ( 0.7071067811865524577, 0.7071067811865425767, -0.000000000000000000 ) ) ;
#11898=ORIENTED_EDGE ( 'NONE', *, *, #8687, .T. ) ;
#11905=LINE ( 'NONE', #12311, #8872 ) ;
#11910=EDGE_LOOP ( 'NONE', ( #12324, #4387, #3173, #5524 ) ) ;
#11915=ORIENTED_EDGE ( 'NONE', *, *, #10970, .F. ) ;
#11922=DIRECTION ( 'NONE',  ( 0.000000000000000000, 0.000000000000000000, 1.000000000000000000 ) ) ;
#11925=LINE ( 'NONE', #13172, #1322 ) ;
#11926=ORIENTED_EDGE ( 'NONE', *, *, #13685, .T. ) ;
#11927=( BOUNDED_CURVE ( )  B_SPLINE_CURVE ( 3, ( #5032, #8524, #10487, #9447 ),
 .UNSPECIFIED., .F., .F. ) 
 B_SPLINE_CURVE_WITH_KNOTS ( ( 4, 4 ),
 ( 1.570796326794896558, 3.141592653589793116 ),
 .UNSPECIFIED. ) 
 CURVE ( )  GEOMETRIC_REPRESENTATION_ITEM ( )  RATIONAL_B_SPLINE_CURVE ( ( 1.000000000000000000, 0.8047378541243649375, 0.8047378541243649375, 1.000000000000000000 ) ) 
 REPRESENTATION_ITEM ( '' )  );
#11929=VERTEX_POINT ( 'NONE', #4820 ) ;
#11935=CARTESIAN_POINT ( 'NONE',  ( 185.2712718049083946, 104.1554980190242361, 23.00000000000000000 ) ) ;
#11940=LINE ( 'NONE', #2325, #5146 ) ;
#11955=FACE_OUTER_BOUND ( 'NONE', #4645, .T. ) ;
#11964=DIRECTION ( 'NONE',  ( 1.000000000000000000, 0.000000000000000000, 0.000000000000000000 ) ) ;
#11970=CARTESIAN_POINT ( 'NONE',  ( 98.27605811426136029, 115.9375248198690826, 20.00000000000000000 ) ) ;
#11972=CYLINDRICAL_SURFACE ( 'NONE', #9590, 2.000000000000001776 ) ;
#11976=CARTESIAN_POINT ( 'NONE',  ( 42.63563590245419732, 85.03908161011133870, 20.00000000000000000 ) ) ;
#11983=VECTOR ( 'NONE', #4312, 999.9999999999998863 ) ;
#11986=DIRECTION ( 'NONE',  ( -1.000000000000000000, 0.000000000000000000, 0.000000000000000000 ) ) ;
#11990=EDGE_CURVE ( 'NONE', #6295, #3941, #5651, .T. ) ;
#11991=ADVANCED_FACE ( 'NONE', ( #5920 ), #11256, .T. ) ;
#11992=ADVANCED_FACE ( 'NONE', ( #7888 ), #2001, .T. ) ;
#12005=CARTESIAN_POINT ( 'NONE',  ( 134.6356359024541973, 94.90549801902425031, 20.00000000000000000 ) ) ;
#12009=AXIS2_PLACEMENT_3D ( 'NONE', #12778, #5428, #4335 ) ;
#12012=EDGE_LOOP ( 'NONE', ( #5628, #9315, #5757, #6222 ) ) ;
#12014=AXIS2_PLACEMENT_3D ( 'NONE', #9450, #13754, #8391 ) ;
#12020=DIRECTION ( 'NONE',  ( 1.000000000000000000, 0.000000000000000000, -0.000000000000000000 ) ) ;
#12024=DIRECTION ( 'NONE',  ( -0.000000000000000000, -0.000000000000000000, 1.000000000000000000 ) ) ;
#12027=AXIS2_PLACEMENT_3D ( 'NONE', #9960, #7852, #2578 ) ;
#12030=EDGE_CURVE ( 'NONE', #2858, #1798, #3567, .T. ) ;
#12031=CARTESIAN_POINT ( 'NONE',  ( 142.3249757306743675, 110.9104019536709274, 19.99999999999999289 ) ) ;
#12036=CARTESIAN_POINT ( 'NONE',  ( 142.6356359024541973, 87.03908161011133870, 20.00000000000000000 ) ) ;
#12042=VECTOR ( 'NONE', #11653, 1000.000000000000000 ) ;
#12045=AXIS2_PLACEMENT_3D ( 'NONE', #6887, #11092, #7713 ) ;
#12048=EDGE_CURVE ( 'NONE', #8944, #9587, #12901, .T. ) ;
#12056=DIRECTION ( 'NONE',  ( 0.000000000000000000, 0.000000000000000000, 1.000000000000000000 ) ) ;
#12060=AXIS2_PLACEMENT_3D ( 'NONE', #3445, #12024, #2478 ) ;
#12072=CARTESIAN_POINT ( 'NONE',  ( 140.6356359024541973, 90.15549801902423610, 23.00000000000000000 ) ) ;
#12073=EDGE_CURVE ( 'NONE', #2221, #1954, #12431, .T. ) ;
#12074=CARTESIAN_POINT ( 'NONE',  ( 140.6356359024541973, 113.0390816101113387, 19.25000000000000000 ) ) ;
#12076=EDGE_CURVE ( 'NONE', #12394, #5520, #8991, .T. ) ;
#12077=FACE_OUTER_BOUND ( 'NONE', #12534, .T. ) ;
#12087=DIRECTION ( 'NONE',  ( 0.000000000000000000, 0.000000000000000000, 1.000000000000000000 ) ) ;
#12090=DIRECTION ( 'NONE',  ( 1.000000000000000000, 0.000000000000000000, 0.000000000000000000 ) ) ;
#12098=EDGE_CURVE ( 'NONE', #3533, #1109, #691, .T. ) ;
#12104=ORIENTED_EDGE ( 'NONE', *, *, #12977, .T. ) ;
#12110=EDGE_CURVE ( 'NONE', #7324, #4724, #6870, .T. ) ;
#12118=EDGE_LOOP ( 'NONE', ( #1054, #9520, #4906, #13221 ) ) ;
#12120=ORIENTED_EDGE ( 'NONE', *, *, #11842, .F. ) ;
#12122=PLANE ( 'NONE',  #11741 ) ;
#12128=CARTESIAN_POINT ( 'NONE',  ( 109.6856792294029219, 115.9888905337886769, 0.7500000000000006661 ) ) ;
#12138=VERTEX_POINT ( 'NONE', #3855 ) ;
#12139=CARTESIAN_POINT ( 'NONE',  ( 92.63563590245421153, 99.03908161011133870, 20.00000000000000000 ) ) ;
#12140=CARTESIAN_POINT ( 'NONE',  ( 109.1537879975201406, 115.4601262030644762, 20.00000000000000000 ) ) ;
#12145=DIRECTION ( 'NONE',  ( 0.000000000000000000, 0.000000000000000000, 1.000000000000000000 ) ) ;
#12147=ORIENTED_EDGE ( 'NONE', *, *, #6132, .T. ) ;
#12149=DIRECTION ( 'NONE',  ( 1.000000000000000000, 0.000000000000000000, 0.000000000000000000 ) ) ;
#12150=DIRECTION ( 'NONE',  ( 1.000000000000000000, -0.000000000000000000, -0.000000000000000000 ) ) ;
#12152=CARTESIAN_POINT ( 'NONE',  ( 109.1537879975201406, 82.61803701715820125, 0.7500000000000000000 ) ) ;
#12159=DIRECTION ( 'NONE',  ( 1.000000000000000000, 0.000000000000000000, 0.000000000000000000 ) ) ;
#12164=CARTESIAN_POINT ( 'NONE',  ( 102.2760581142613603, 115.9375248198690826, 10.00000000000000000 ) ) ;
#12176=VERTEX_POINT ( 'NONE', #8168 ) ;
#12177=DIRECTION ( 'NONE',  ( 0.000000000000000000, -0.000000000000000000, -1.000000000000000000 ) ) ;
#12178=DIRECTION ( 'NONE',  ( 1.000000000000000000, 0.000000000000000000, 0.000000000000000000 ) ) ;
#12183=EDGE_CURVE ( 'NONE', #939, #6125, #9292, .T. ) ;
#12191=CARTESIAN_POINT ( 'NONE',  ( 109.6856792294029219, 82.08927268643400055, 20.00000000000000000 ) ) ;
#12194=DIRECTION ( 'NONE',  ( -0.7050191076322684935, 0.7091883091770477821, 0.000000000000000000 ) ) ;
#12198=VERTEX_POINT ( 'NONE', #3429 ) ;
#12202=FACE_OUTER_BOUND ( 'NONE', #6139, .T. ) ;
#12206=EDGE_CURVE ( 'NONE', #7886, #13749, #11726, .T. ) ;
#12213=PLANE ( 'NONE',  #9172 ) ;
#12217=ORIENTED_EDGE ( 'NONE', *, *, #7150, .T. ) ;
#12220=ORIENTED_EDGE ( 'NONE', *, *, #11835, .F. ) ;
#12222=EDGE_CURVE ( 'NONE', #135, #8835, #4194, .T. ) ;
#12223=LINE ( 'NONE', #13330, #9 ) ;
#12228=VECTOR ( 'NONE', #8342, 1000.000000000000000 ) ;
#12243=FACE_OUTER_BOUND ( 'NONE', #5913, .T. ) ;
#12244=DIRECTION ( 'NONE',  ( 0.000000000000000000, -0.000000000000000000, 1.000000000000000000 ) ) ;
#12247=CIRCLE ( 'NONE', #13353, 0.7499999999999966693 ) ;
#12250=CIRCLE ( 'NONE', #13781, 0.7500000000000006661 ) ;
#12253=VECTOR ( 'NONE', #7638, 999.9999999999998863 ) ;
#12258=DIRECTION ( 'NONE',  ( -1.000000000000000000, -0.000000000000000000, -0.000000000000000000 ) ) ;
#12259=ORIENTED_EDGE ( 'NONE', *, *, #11392, .F. ) ;
#12263=DIRECTION ( 'NONE',  ( 1.000000000000000000, 0.000000000000000000, 0.000000000000000000 ) ) ;
#12266=DIRECTION ( 'NONE',  ( 1.000000000000000000, 0.000000000000000000, 0.000000000000000000 ) ) ;
#12268=CARTESIAN_POINT ( 'NONE',  ( 76.11748380738829667, 82.61803701715820125, 0.7500000000000000000 ) ) ;
#12269=ADVANCED_FACE ( 'NONE', ( #10754 ), #4394, .T. ) ;
#12279=CARTESIAN_POINT ( 'NONE',  ( 44.63563590245422574, 113.0390816101113387, 19.25000000000000000 ) ) ;
#12289=CARTESIAN_POINT ( 'NONE',  ( 109.6856792294029219, 82.08927268643400055, 0.7500000000000006661 ) ) ;
#12307=ADVANCED_FACE ( 'NONE', ( #13254 ), #2738, .T. ) ;
#12309=SHAPE_REPRESENTATION ( 'Central Rotary Housing', ( #6434 ), #5310 ) ;
#12311=CARTESIAN_POINT ( 'NONE',  ( 134.6356359024541973, 94.65549801902425031, 23.00000000000000000 ) ) ;
#12314=PLANE ( 'NONE',  #4261 ) ;
#12318=CIRCLE ( 'NONE', #6289, 23.29163056034261459 ) ;
#12324=ORIENTED_EDGE ( 'NONE', *, *, #8339, .F. ) ;
#12344=DIRECTION ( 'NONE',  ( 0.000000000000000000, 0.000000000000000000, 1.000000000000000000 ) ) ;
#12346=ADVANCED_FACE ( 'NONE', ( #8857 ), #7307, .T. ) ;
#12350=ORIENTED_EDGE ( 'NONE', *, *, #10998, .F. ) ;
#12352=DIRECTION ( 'NONE',  ( -0.000000000000000000, 1.000000000000000000, -0.000000000000000000 ) ) ;
#12358=CYLINDRICAL_SURFACE ( 'NONE', #1312, 0.2500000000000002220 ) ;
#12363=EDGE_CURVE ( 'NONE', #363, #939, #7937, .T. ) ;
#12366=ORIENTED_EDGE ( 'NONE', *, *, #13723, .F. ) ;
#12368=CARTESIAN_POINT ( 'NONE',  ( 42.63563590245419732, 112.2890816101113387, 0.7500000000000006661 ) ) ;
#12374=DIRECTION ( 'NONE',  ( 0.000000000000000000, 0.000000000000000000, 1.000000000000000000 ) ) ;
#12380=VERTEX_POINT ( 'NONE', #8013 ) ;
#12390=DIRECTION ( 'NONE',  ( -0.7071067811865524577, -0.7071067811865425767, 0.000000000000000000 ) ) ;
#12392=EDGE_LOOP ( 'NONE', ( #6103, #6153, #12366, #9537 ) ) ;
#12394=VERTEX_POINT ( 'NONE', #543 ) ;
#12405=ORIENTED_EDGE ( 'NONE', *, *, #13296, .T. ) ;
#12406=DIRECTION ( 'NONE',  ( 0.000000000000000000, -0.000000000000000000, 1.000000000000000000 ) ) ;
#12409=DIRECTION ( 'NONE',  ( 0.000000000000000000, 0.000000000000000000, 1.000000000000000000 ) ) ;
#12415=CARTESIAN_POINT ( 'NONE',  ( 92.63563590245421153, 99.03908161011133870, 20.00000000000000000 ) ) ;
#12429=DIRECTION ( 'NONE',  ( 0.000000000000000000, 0.000000000000000000, 1.000000000000000000 ) ) ;
#12431=LINE ( 'NONE', #13680, #6880 ) ;
#12432=CARTESIAN_POINT ( 'NONE',  ( 50.63563590245420443, 108.9054980190242503, 23.00000000000000000 ) ) ;
#12437=ORIENTED_EDGE ( 'NONE', *, *, #9064, .T. ) ;
#12449=LINE ( 'NONE', #10297, #11170 ) ;
#12450=DIRECTION ( 'NONE',  ( 0.000000000000000000, 0.000000000000000000, 1.000000000000000000 ) ) ;
#12460=VERTEX_POINT ( 'NONE', #6182 ) ;
#12462=AXIS2_PLACEMENT_3D ( 'NONE', #3103, #4974, #8180 ) ;
#12463=EDGE_LOOP ( 'NONE', ( #3700, #1165, #1382, #6297 ) ) ;
#12464=TOROIDAL_SURFACE ( 'NONE', #5989, 10.75000000000000000, 0.7500000000000000000 ) ;
#12471=FACE_BOUND ( 'NONE', #7631, .T. ) ;
#12476=CARTESIAN_POINT ( 'NONE',  ( 68.49370948373500312, 123.0390816101113245, 20.00000000000000000 ) ) ;
#12486=CARTESIAN_POINT ( 'NONE',  ( 140.6356359024541973, 108.9054980190242503, 22.75000000000000000 ) ) ;
#12487=AXIS2_PLACEMENT_3D ( 'NONE', #11338, #3876, #4085 ) ;
#12488=CARTESIAN_POINT ( 'NONE',  ( 50.38563590245420443, 108.6554980190242503, 23.00000000000000000 ) ) ;
#12490=ADVANCED_FACE ( 'NONE', ( #13391 ), #12624, .F. ) ;
#12493=CARTESIAN_POINT ( 'NONE',  ( 86.99521369064697751, 82.14063840035363739, 10.00000000000000000 ) ) ;
#12503=FACE_OUTER_BOUND ( 'NONE', #6027, .T. ) ;
#12512=EDGE_CURVE ( 'NONE', #209, #1798, #5539, .T. ) ;
#12514=CARTESIAN_POINT ( 'NONE',  ( 140.6356359024541973, 103.9054980190242361, 20.00000000000000000 ) ) ;
#12533=EDGE_LOOP ( 'NONE', ( #5334, #9129, #2069, #11784 ) ) ;
#12534=EDGE_LOOP ( 'NONE', ( #11188, #4102, #12839, #5369 ) ) ;
#12543=CARTESIAN_POINT ( 'NONE',  ( 72.18094369249178044, 97.20665973629650125, 10.00000000000000000 ) ) ;
#12550=AXIS2_PLACEMENT_3D ( 'NONE', #2803, #8217, #11235 ) ;
#12556=CARTESIAN_POINT ( 'NONE',  ( 44.63563590245421864, 85.03908161011133870, 20.00000000000000000 ) ) ;
#12559=ORIENTED_EDGE ( 'NONE', *, *, #1915, .T. ) ;
#12561=CARTESIAN_POINT ( 'NONE',  ( 50.38563590245420443, 90.15549801902423610, 23.00000000000000000 ) ) ;
#12565=DIRECTION ( 'NONE',  ( -0.7050191076322684935, -0.7091883091770477821, -0.000000000000000000 ) ) ;
#12568=VERTEX_POINT ( 'NONE', #12561 ) ;
#12570=ORIENTED_EDGE ( 'NONE', *, *, #13055, .F. ) ;
#12576=DIRECTION ( 'NONE',  ( -1.000000000000000000, 0.000000000000000000, 0.000000000000000000 ) ) ;
#12577=ADVANCED_FACE ( 'NONE', ( #8150 ), #12358, .T. ) ;
#12588=ORIENTED_EDGE ( 'NONE', *, *, #3229, .T. ) ;
#12593=CARTESIAN_POINT ( 'NONE',  ( 116.7775623211734342, 113.0390816101113387, 19.25000000000000000 ) ) ;
#12600=ORIENTED_EDGE ( 'NONE', *, *, #9214, .F. ) ;
#12601=EDGE_LOOP ( 'NONE', ( #764, #2920, #7495, #1841 ) ) ;
#12611=EDGE_CURVE ( 'NONE', #3610, #13231, #9123, .T. ) ;
#12615=DIRECTION ( 'NONE',  ( -1.000000000000000000, 0.000000000000000000, 0.000000000000000000 ) ) ;
#12624=CYLINDRICAL_SURFACE ( 'NONE', #11120, 2.000000000000001776 ) ;
#12630=VERTEX_POINT ( 'NONE', #45 ) ;
#12634=DIRECTION ( 'NONE',  ( 1.000000000000000000, 0.000000000000000000, 0.000000000000000000 ) ) ;
#12643=CARTESIAN_POINT ( 'NONE',  ( 134.7391892930474739, 108.8019446284309737, 23.00000000000000000 ) ) ;
#12644=CARTESIAN_POINT ( 'NONE',  ( 134.6356359024541973, 94.90549801902423610, 22.89644660940672694 ) ) ;
#12651=CYLINDRICAL_SURFACE ( 'NONE', #7939, 0.2500000000000002220 ) ;
#12661=CARTESIAN_POINT ( 'NONE',  ( 142.6356359024541973, 85.03908161011133870, 0.7500000000000006661 ) ) ;
#12666=EDGE_CURVE ( 'NONE', #3713, #4189, #8001, .T. ) ;
#12669=DIRECTION ( 'NONE',  ( 1.000000000000000000, 0.000000000000000000, 0.000000000000000000 ) ) ;
#12670=EDGE_LOOP ( 'NONE', ( #11275, #8697, #10168, #11926 ) ) ;
#12671=CARTESIAN_POINT ( 'NONE',  ( 44.88563590245420443, 94.65549801902425031, 23.00000000000000000 ) ) ;
#12677=VECTOR ( 'NONE', #1419, 1000.000000000000000 ) ;
#12682=ORIENTED_EDGE ( 'NONE', *, *, #12222, .T. ) ;
#12684=DIRECTION ( 'NONE',  ( -0.000000000000000000, -0.000000000000000000, 1.000000000000000000 ) ) ;
#12685=ORIENTED_EDGE ( 'NONE', *, *, #8612, .F. ) ;
#12687=EDGE_CURVE ( 'NONE', #6660, #3775, #3730, .T. ) ;
#12692=CARTESIAN_POINT ( 'NONE',  ( 44.73918929304747394, 104.0090514096174843, 23.00000000000000000 ) ) ;
#12696=EDGE_CURVE ( 'NONE', #10605, #3613, #8625, .T. ) ;
#12697=FACE_OUTER_BOUND ( 'NONE', #1474, .T. ) ;
#12702=VERTEX_POINT ( 'NONE', #12887 ) ;
#12704=ADVANCED_FACE ( 'NONE', ( #11853 ), #2304, .T. ) ;
#12705=LINE ( 'NONE', #13738, #1945 ) ;
#12738=VERTEX_POINT ( 'NONE', #4176 ) ;
#12739=ORIENTED_EDGE ( 'NONE', *, *, #2631, .F. ) ;
#12742=DIRECTION ( 'NONE',  ( 0.000000000000000000, 0.000000000000000000, 1.000000000000000000 ) ) ;
#12747=LINE ( 'NONE', #8547, #1145 ) ;
#12756=DIRECTION ( 'NONE',  ( 0.7091883091770476710, -0.7050191076322684935, 0.000000000000000000 ) ) ;
#12760=FACE_OUTER_BOUND ( 'NONE', #6136, .T. ) ;
#12763=CARTESIAN_POINT ( 'NONE',  ( 140.6356359024541973, 85.03908161011132449, 19.68933982822018081 ) ) ;
#12767=EDGE_CURVE ( 'NONE', #9970, #8747, #6339, .T. ) ;
#12770=EDGE_LOOP ( 'NONE', ( #371, #2622, #449, #9596 ) ) ;
#12772=ORIENTED_EDGE ( 'NONE', *, *, #13444, .T. ) ;
#12778=CARTESIAN_POINT ( 'NONE',  ( 92.63563590245421153, 112.2890816101113387, 19.25000000000000000 ) ) ;
#12779=CARTESIAN_POINT ( 'NONE',  ( 68.49370948373500312, 85.03908161011133870, 0.7500000000000006661 ) ) ;
#12784=ORIENTED_EDGE ( 'NONE', *, *, #770, .F. ) ;
#12792=AXIS2_PLACEMENT_3D ( 'NONE', #10195, #1811, #680 ) ;
#12795=ADVANCED_FACE ( 'NONE', ( #7639 ), #9904, .T. ) ;
#12800=ORIENTED_EDGE ( 'NONE', *, *, #8529, .F. ) ;
#12801=ADVANCED_FACE ( 'NONE', ( #7704 ), #12464, .T. ) ;
#12807=LINE ( 'NONE', #1138, #1967 ) ;
#12808=DIRECTION ( 'NONE',  ( 1.000000000000000000, 0.000000000000000000, 0.000000000000000000 ) ) ;
#12819=DIRECTION ( 'NONE',  ( -0.000000000000000000, -0.000000000000000000, 1.000000000000000000 ) ) ;
#12820=( BOUNDED_CURVE ( )  B_SPLINE_CURVE ( 3, ( #7126, #6994, #8181, #10354 ),
 .UNSPECIFIED., .F., .T. ) 
 B_SPLINE_CURVE_WITH_KNOTS ( ( 4, 4 ),
 ( 1.570796326794896558, 3.141592653589793560 ),
 .UNSPECIFIED. ) 
 CURVE ( )  GEOMETRIC_REPRESENTATION_ITEM ( )  RATIONAL_B_SPLINE_CURVE ( ( 1.000000000000000000, 0.8047378541243649375, 0.8047378541243649375, 1.000000000000000000 ) ) 
 REPRESENTATION_ITEM ( '' )  );
#12821=FACE_OUTER_BOUND ( 'NONE', #9461, .T. ) ;
#12825=DIRECTION ( 'NONE',  ( 0.000000000000000000, 0.000000000000000000, 1.000000000000000000 ) ) ;
#12832=EDGE_CURVE ( 'NONE', #10749, #6706, #12250, .T. ) ;
#12837=AXIS2_PLACEMENT_3D ( 'NONE', #10587, #3134, #3328 ) ;
#12839=ORIENTED_EDGE ( 'NONE', *, *, #8464, .F. ) ;
#12843=ORIENTED_EDGE ( 'NONE', *, *, #6104, .T. ) ;
#12845=CARTESIAN_POINT ( 'NONE',  ( 109.6856792294029219, 115.9888905337886769, 20.00000000000000000 ) ) ;
#12850=EDGE_CURVE ( 'NONE', #6180, #2221, #10952, .T. ) ;
#12857=APPLICATION_CONTEXT ( 'automotive_design' ) ;
#12860=VERTEX_POINT ( 'NONE', #5624 ) ;
#12863=ORIENTED_EDGE ( 'NONE', *, *, #2712, .F. ) ;
#12864=CARTESIAN_POINT ( 'NONE',  ( 111.0903281124166710, 100.8715034839261762, 10.00000000000000000 ) ) ;
#12865=DIRECTION ( 'NONE',  ( 1.000000000000000000, 0.000000000000000000, 0.000000000000000000 ) ) ;
#12874=SHAPE_DEFINITION_REPRESENTATION ( #2602, #12309 ) ;
#12881=CARTESIAN_POINT ( 'NONE',  ( 74.18094369249178044, 97.20665973629650125, 20.00000000000000000 ) ) ;
#12887=CARTESIAN_POINT ( 'NONE',  ( 44.88563590245420443, 90.15549801902423610, 23.00000000000000000 ) ) ;
#12900=DIRECTION ( 'NONE',  ( 0.000000000000000000, -1.000000000000000000, 0.000000000000000000 ) ) ;
#12901=CIRCLE ( 'NONE', #5538, 2.000000000000001776 ) ;
#12909=PRODUCT_DEFINITION_FORMATION_WITH_SPECIFIED_SOURCE ( 'ANY', '', #2255, .NOT_KNOWN. ) ;
#12911=EDGE_CURVE ( 'NONE', #2972, #363, #8200, .T. ) ;
#12918=CARTESIAN_POINT ( 'NONE',  ( 42.63563590245419732, 113.0390816101113387, 0.7500000000000006661 ) ) ;
#12919=LINE ( 'NONE', #4876, #5533 ) ;
#12920=FACE_OUTER_BOUND ( 'NONE', #3913, .T. ) ;
#12921=CARTESIAN_POINT ( 'NONE',  ( 111.0903281124166710, 100.8715034839261762, 10.00000000000000000 ) ) ;
#12922=AXIS2_PLACEMENT_3D ( 'NONE', #5441, #2062, #2273 ) ;
#12923=CIRCLE ( 'NONE', #11150, 10.74999999999999645 ) ;
#12929=CARTESIAN_POINT ( 'NONE',  ( 62.16596598834446752, 129.5087515242215090, 19.25000000000000000 ) ) ;
#12934=CIRCLE ( 'NONE', #2047, 2.000000000000001776 ) ;
#12940=DIRECTION ( 'NONE',  ( -0.000000000000000000, -0.000000000000000000, -1.000000000000000000 ) ) ;
#12941=CARTESIAN_POINT ( 'NONE',  ( 44.63563590245422574, 113.0390816101113387, 19.25000000000000000 ) ) ;
#12942=EDGE_CURVE ( 'NONE', #4724, #4825, #6861, .T. ) ;
#12943=CARTESIAN_POINT ( 'NONE',  ( 109.1537879975201406, 82.61803701715820125, 19.25000000000000000 ) ) ;
#12948=VECTOR ( 'NONE', #6019, 1000.000000000000000 ) ;
#12956=CARTESIAN_POINT ( 'NONE',  ( 50.63563590245420443, 108.9054980190242503, 22.75000000000000000 ) ) ;
#12972=EDGE_LOOP ( 'NONE', ( #10257, #9604, #10971, #772 ) ) ;
#12975=ORIENTED_EDGE ( 'NONE', *, *, #10700, .T. ) ;
#12977=EDGE_CURVE ( 'NONE', #9491, #2697, #1788, .T. ) ;
#12986=UNCERTAINTY_MEASURE_WITH_UNIT (LENGTH_MEASURE( 1.000000000000000082E-05 ), #2098, 'distance_accuracy_value', 'NONE');
#12996=DIRECTION ( 'NONE',  ( -0.000000000000000000, -1.000000000000000000, -0.000000000000000000 ) ) ;
#13006=EDGE_LOOP ( 'NONE', ( #7481, #3361, #7963, #4059 ) ) ;
#13009=FACE_OUTER_BOUND ( 'NONE', #10596, .T. ) ;
#13040=CARTESIAN_POINT ( 'NONE',  ( 44.63563590245420443, 103.9054980190242361, 23.00000000000000000 ) ) ;
#13046=DIRECTION ( 'NONE',  ( -0.000000000000000000, -0.000000000000000000, 1.000000000000000000 ) ) ;
#13052=LINE ( 'NONE', #200, #3312 ) ;
#13055=EDGE_CURVE ( 'NONE', #4825, #9584, #2286, .T. ) ;
#13059=ORIENTED_EDGE ( 'NONE', *, *, #10181, .T. ) ;
#13063=CYLINDRICAL_SURFACE ( 'NONE', #8053, 0.7500000000000000000 ) ;
#13064=CARTESIAN_POINT ( 'NONE',  ( 140.6356359024541973, 89.90549801902423610, 22.75000000000000000 ) ) ;
#13067=ADVANCED_FACE ( 'NONE', ( #945 ), #5457, .T. ) ;
#13070=ORIENTED_EDGE ( 'NONE', *, *, #9831, .F. ) ;
#13074=ORIENTED_EDGE ( 'NONE', *, *, #3418, .F. ) ;
#13076=VERTEX_POINT ( 'NONE', #10789 ) ;
#13087=ORIENTED_EDGE ( 'NONE', *, *, #12048, .T. ) ;
#13090=DIRECTION ( 'NONE',  ( -0.000000000000000000, -0.000000000000000000, 1.000000000000000000 ) ) ;
#13091=ADVANCED_FACE ( 'NONE', ( #11757 ), #2079, .T. ) ;
#13093=DIRECTION ( 'NONE',  ( -0.000000000000000000, 0.000000000000000000, 1.000000000000000000 ) ) ;
#13096=DIRECTION ( 'NONE',  ( 0.000000000000000000, 0.000000000000000000, 1.000000000000000000 ) ) ;
#13102=ADVANCED_FACE ( 'NONE', ( #11698 ), #10645, .T. ) ;
#13109=EDGE_CURVE ( 'NONE', #3193, #8675, #1053, .T. ) ;
#13110=CARTESIAN_POINT ( 'NONE',  ( 44.63563590245421864, 85.03908161011133870, 20.00000000000000000 ) ) ;
#13121=VECTOR ( 'NONE', #12669, 1000.000000000000000 ) ;
#13123=EDGE_CURVE ( 'NONE', #10749, #10483, #12807, .T. ) ;
#13131=DIRECTION ( 'NONE',  ( -0.7050191076322684935, 0.7091883091770476710, 0.000000000000000000 ) ) ;
#13138=AXIS2_PLACEMENT_3D ( 'NONE', #6631, #11808, #10697 ) ;
#13139=CIRCLE ( 'NONE', #10897, 2.000000000000001776 ) ;
#13151=DIRECTION ( 'NONE',  ( 0.000000000000000000, -1.000000000000000000, 0.000000000000000000 ) ) ;
#13155=CARTESIAN_POINT ( 'NONE',  ( 140.3856359024541973, 90.15549801902423610, 23.00000000000000000 ) ) ;
#13157=EDGE_LOOP ( 'NONE', ( #13748, #12772 ) ) ;
#13158=AXIS2_PLACEMENT_3D ( 'NONE', #9128, #7928, #535 ) ;
#13168=DIRECTION ( 'NONE',  ( -1.000000000000000000, -0.000000000000000000, -0.000000000000000000 ) ) ;
#13171=LINE ( 'NONE', #7782, #1127 ) ;
#13172=CARTESIAN_POINT ( 'NONE',  ( 50.63563590245420443, 103.9054980190242361, 20.00000000000000000 ) ) ;
#13173=VECTOR ( 'NONE', #3631, 1000.000000000000000 ) ;
#13179=CIRCLE ( 'NONE', #4272, 0.7500000000000006661 ) ;
#13180=DIRECTION ( 'NONE',  ( 1.000000000000000000, 0.000000000000000000, 0.000000000000000000 ) ) ;
#13184=LINE ( 'NONE', #8995, #13173 ) ;
#13191=DIRECTION ( 'NONE',  ( 0.000000000000000000, 0.000000000000000000, 1.000000000000000000 ) ) ;
#13199=DIRECTION ( 'NONE',  ( -0.000000000000000000, -0.000000000000000000, -1.000000000000000000 ) ) ;
#13201=EDGE_LOOP ( 'NONE', ( #9442, #2993, #3218, #13597 ) ) ;
#13203=CARTESIAN_POINT ( 'NONE',  ( 134.6356359024541973, 103.9054980190242361, 22.89644660940672694 ) ) ;
#13205=CARTESIAN_POINT ( 'NONE',  ( 140.6356359024541689, 85.03908161011133870, 0.7500000000000006661 ) ) ;
#13207=DIRECTION ( 'NONE',  ( 0.000000000000000000, -1.000000000000000000, 0.000000000000000000 ) ) ;
#13215=EDGE_LOOP ( 'NONE', ( #10313, #1939, #12217, #13059 ) ) ;
#13218=VERTEX_POINT ( 'NONE', #5791 ) ;
#13221=ORIENTED_EDGE ( 'NONE', *, *, #12977, .F. ) ;
#13224=LINE ( 'NONE', #3665, #3752 ) ;
#13226=DIRECTION ( 'NONE',  ( -0.000000000000000000, -0.000000000000000000, 1.000000000000000000 ) ) ;
#13229=EDGE_CURVE ( 'NONE', #1301, #4724, #7503, .T. ) ;
#13231=VERTEX_POINT ( 'NONE', #9074 ) ;
#13232=EDGE_CURVE ( 'NONE', #11929, #719, #11905, .T. ) ;
#13234=ORIENTED_EDGE ( 'NONE', *, *, #10084, .T. ) ;
#13240=CARTESIAN_POINT ( 'NONE',  ( 50.63563590245420443, 103.9054980190242361, 22.75000000000000000 ) ) ;
#13247=DIRECTION ( 'NONE',  ( 1.000000000000000000, 0.000000000000000000, 0.000000000000000000 ) ) ;
#13251=CARTESIAN_POINT ( 'NONE',  ( 62.16596598834396303, 68.56941169600129626, 0.7500000000000000000 ) ) ;
#13254=FACE_OUTER_BOUND ( 'NONE', #2100, .T. ) ;
#13259=CARTESIAN_POINT ( 'NONE',  ( 43.38563590245419732, 110.7284214383315089, 0.000000000000000000 ) ) ;
#13260=EDGE_CURVE ( 'NONE', #10544, #11762, #3767, .T. ) ;
#13264=FACE_OUTER_BOUND ( 'NONE', #5221, .T. ) ;
#13266=VERTEX_POINT ( 'NONE', #11970 ) ;
#13288=CYLINDRICAL_SURFACE ( 'NONE', #11642, 2.000000000000001776 ) ;
#13294=EDGE_LOOP ( 'NONE', ( #11461, #11662, #3886, #7693 ) ) ;
#13296=EDGE_CURVE ( 'NONE', #6971, #719, #10341, .T. ) ;
#13298=CARTESIAN_POINT ( 'NONE',  ( 68.49370948373500312, 85.03908161011133870, 20.00000000000000000 ) ) ;
#13303=LINE ( 'NONE', #5623, #10655 ) ;
#13304=CARTESIAN_POINT ( 'NONE',  ( 68.49370948373500312, 112.2890816101113387, 19.25000000000000000 ) ) ;
#13305=DIRECTION ( 'NONE',  ( -1.000000000000000000, -0.000000000000000000, -0.000000000000000000 ) ) ;
#13308=EDGE_CURVE ( 'NONE', #9491, #3613, #5672, .T. ) ;
#13322=ADVANCED_FACE ( 'NONE', ( #1827 ), #5023, .T. ) ;
#13323=AXIS2_PLACEMENT_3D ( 'NONE', #11281, #7005, #13572 ) ;
#13326=CARTESIAN_POINT ( 'NONE',  ( 92.63563590245421153, 99.03908161011133870, 20.00000000000000000 ) ) ;
#13327=ORIENTED_EDGE ( 'NONE', *, *, #3990, .F. ) ;
#13329=CARTESIAN_POINT ( 'NONE',  ( 142.1053058165643108, 110.5087515242214096, 0.000000000000000000 ) ) ;
#13330=CARTESIAN_POINT ( 'NONE',  ( 50.63563590245420443, 94.90549801902425031, 22.75000000000000000 ) ) ;
#13331=CIRCLE ( 'NONE', #10445, 2.000000000000001776 ) ;
#13332=DIRECTION ( 'NONE',  ( -0.000000000000000000, -0.000000000000000000, -1.000000000000000000 ) ) ;
#13353=AXIS2_PLACEMENT_3D ( 'NONE', #12152, #12565, #13595 ) ;
#13358=CARTESIAN_POINT ( 'NONE',  ( 134.8856359024541973, 89.90549801902423610, 23.00000000000000000 ) ) ;
#13363=CARTESIAN_POINT ( 'NONE',  ( 50.63563590245420443, 94.65549801902425031, 22.75000000000000000 ) ) ;
#13370=LINE ( 'NONE', #7072, #2989 ) ;
#13388=LINE ( 'NONE', #3837, #8518 ) ;
#13391=FACE_OUTER_BOUND ( 'NONE', #251, .T. ) ;
#13393=CARTESIAN_POINT ( 'NONE',  ( 50.38563590245420443, 94.65549801902425031, 23.00000000000000000 ) ) ;
#13395=EDGE_CURVE ( 'NONE', #11676, #3610, #4963, .T. ) ;
#13397=AXIS2_PLACEMENT_3D ( 'NONE', #10804, #9089, #3792 ) ;
#13404=ORIENTED_EDGE ( 'NONE', *, *, #9449, .F. ) ;
#13410=DIRECTION ( 'NONE',  ( 0.000000000000000000, 0.000000000000000000, 1.000000000000000000 ) ) ;
#13411=VECTOR ( 'NONE', #9155, 1000.000000000000000 ) ;
#13415=DIRECTION ( 'NONE',  ( -0.000000000000000000, 0.000000000000000000, -1.000000000000000000 ) ) ;
#13428=DIRECTION ( 'NONE',  ( -1.000000000000000000, 0.000000000000000000, -0.000000000000000000 ) ) ;
#13435=( BOUNDED_CURVE ( )  B_SPLINE_CURVE ( 3, ( #10590, #102, #8556, #3332 ),
 .UNSPECIFIED., .F., .F. ) 
 B_SPLINE_CURVE_WITH_KNOTS ( ( 4, 4 ),
 ( 1.570796326794896558, 3.141592653589793560 ),
 .UNSPECIFIED. ) 
 CURVE ( )  GEOMETRIC_REPRESENTATION_ITEM ( )  RATIONAL_B_SPLINE_CURVE ( ( 1.000000000000000000, 0.8047378541243649375, 0.8047378541243649375, 1.000000000000000000 ) ) 
 REPRESENTATION_ITEM ( '' )  );
#13438=ADVANCED_FACE ( 'NONE', ( #12503 ), #9439, .T. ) ;
#13439=EDGE_LOOP ( 'NONE', ( #13087, #2456 ) ) ;
#13444=EDGE_CURVE ( 'NONE', #13530, #11751, #13331, .T. ) ;
#13449=EDGE_CURVE ( 'NONE', #11622, #9491, #13052, .T. ) ;
#13460=CARTESIAN_POINT ( 'NONE',  ( 134.7391892930474739, 90.00905140961751272, 23.00000000000000000 ) ) ;
#13465=CARTESIAN_POINT ( 'NONE',  ( 50.63563590245420443, 94.90549801902423610, 22.89644660940672694 ) ) ;
#13466=CARTESIAN_POINT ( 'NONE',  ( 81.82136590429890077, 114.1051029460540605, 10.00000000000000000 ) ) ;
#13469=ORIENTED_EDGE ( 'NONE', *, *, #3063, .F. ) ;
#13473=ORIENTED_EDGE ( 'NONE', *, *, #5404, .T. ) ;
#13477=DIRECTION ( 'NONE',  ( -0.000000000000000000, -0.000000000000000000, 1.000000000000000000 ) ) ;
#13485=ORIENTED_EDGE ( 'NONE', *, *, #2571, .T. ) ;
#13487=ORIENTED_EDGE ( 'NONE', *, *, #11392, .T. ) ;
#13504=DIRECTION ( 'NONE',  ( 1.000000000000000000, 0.000000000000000000, 0.000000000000000000 ) ) ;
#13514=DIRECTION ( 'NONE',  ( -0.000000000000000000, -0.000000000000000000, -1.000000000000000000 ) ) ;
#13520=CARTESIAN_POINT ( 'NONE',  ( 102.2760581142613603, 115.9375248198690826, 10.00000000000000000 ) ) ;
#13529=ADVANCED_FACE ( 'NONE', ( #11795 ), #1318, .T. ) ;
#13530=VERTEX_POINT ( 'NONE', #283 ) ;
#13533=CARTESIAN_POINT ( 'NONE',  ( 44.63563590245419732, 89.90549801902423610, 22.89644660940672694 ) ) ;
#13540=CARTESIAN_POINT ( 'NONE',  ( 50.63563590245420443, 108.9054980190242503, 20.00000000000000000 ) ) ;
#13545=VERTEX_POINT ( 'NONE', #12779 ) ;
#13551=EDGE_LOOP ( 'NONE', ( #6982, #10945, #5016, #245 ) ) ;
#13555=ORIENTED_EDGE ( 'NONE', *, *, #1310, .T. ) ;
#13557=LINE ( 'NONE', #2771, #5101 ) ;
#13559=CARTESIAN_POINT ( 'NONE',  ( 123.1053058165639555, 68.56941169600116837, 19.25000000000000000 ) ) ;
#13563=AXIS2_PLACEMENT_3D ( 'NONE', #8121, #6928, #1625 ) ;
#13572=DIRECTION ( 'NONE',  ( 1.000000000000000000, 0.000000000000000000, 0.000000000000000000 ) ) ;
#13573=AXIS2_PLACEMENT_3D ( 'NONE', #11809, #74, #10770 ) ;
#13575=PLANE ( 'NONE',  #7598 ) ;
#13594=DIRECTION ( 'NONE',  ( 1.000000000000000000, 0.000000000000000000, 0.000000000000000000 ) ) ;
#13595=DIRECTION ( 'NONE',  ( 0.7091883091770476710, -0.7050191076322684935, 0.000000000000000000 ) ) ;
#13597=ORIENTED_EDGE ( 'NONE', *, *, #6358, .F. ) ;
#13602=VECTOR ( 'NONE', #71, 1000.000000000000000 ) ;
#13611=DIRECTION ( 'NONE',  ( 0.000000000000000000, 0.000000000000000000, -1.000000000000000000 ) ) ;
#13613=DIRECTION ( 'NONE',  ( -0.000000000000000000, 0.000000000000000000, -1.000000000000000000 ) ) ;
#13617=ORIENTED_EDGE ( 'NONE', *, *, #8313, .F. ) ;
#13619=ORIENTED_EDGE ( 'NONE', *, *, #3652, .T. ) ;
#13625=CARTESIAN_POINT ( 'NONE',  ( 134.8856359024541973, 103.9054980190242361, 23.00000000000000000 ) ) ;
#13635=EDGE_CURVE ( 'NONE', #13545, #3128, #7096, .T. ) ;
#13637=( BOUNDED_CURVE ( )  B_SPLINE_CURVE ( 3, ( #453, #10104, #8980, #3676 ),
 .UNSPECIFIED., .F., .F. ) 
 B_SPLINE_CURVE_WITH_KNOTS ( ( 4, 4 ),
 ( 1.570796326794896558, 3.141592653589793116 ),
 .UNSPECIFIED. ) 
 CURVE ( )  GEOMETRIC_REPRESENTATION_ITEM ( )  RATIONAL_B_SPLINE_CURVE ( ( 1.000000000000000000, 0.8047378541243649375, 0.8047378541243649375, 1.000000000000000000 ) ) 
 REPRESENTATION_ITEM ( '' )  );
#13639=VECTOR ( 'NONE', #3952, 1000.000000000000000 ) ;
#13640=VERTEX_POINT ( 'NONE', #6966 ) ;
#13643=ORIENTED_EDGE ( 'NONE', *, *, #2631, .T. ) ;
#13649=DIRECTION ( 'NONE',  ( 0.000000000000000000, 0.000000000000000000, 1.000000000000000000 ) ) ;
#13651=DIRECTION ( 'NONE',  ( 0.000000000000000000, -1.000000000000000000, 0.000000000000000000 ) ) ;
#13652=DIRECTION ( 'NONE',  ( 0.000000000000000000, 0.000000000000000000, 1.000000000000000000 ) ) ;
#13655=ORIENTED_EDGE ( 'NONE', *, *, #3685, .F. ) ;
#13656=ORIENTED_EDGE ( 'NONE', *, *, #12183, .T. ) ;
#13659=ORIENTED_EDGE ( 'NONE', *, *, #1915, .F. ) ;
#13668=LINE ( 'NONE', #5972, #12253 ) ;
#13669=DIRECTION ( 'NONE',  ( 0.000000000000000000, 0.000000000000000000, -1.000000000000000000 ) ) ;
#13672=ORIENTED_EDGE ( 'NONE', *, *, #13723, .T. ) ;
#13675=ORIENTED_EDGE ( 'NONE', *, *, #5766, .T. ) ;
#13680=CARTESIAN_POINT ( 'NONE',  ( 140.6356359024541973, 94.90549801902425031, 20.00000000000000000 ) ) ;
#13681=CARTESIAN_POINT ( 'NONE',  ( 0.000000000000000000, 90.15549801902423610, 22.75000000000000000 ) ) ;
#13685=EDGE_CURVE ( 'NONE', #8747, #9710, #10196, .T. ) ;
#13688=ORIENTED_EDGE ( 'NONE', *, *, #9612, .F. ) ;
#13692=DIRECTION ( 'NONE',  ( 0.7071067811865425767, -0.7071067811865524577, 0.000000000000000000 ) ) ;
#13695=CARTESIAN_POINT ( 'NONE',  ( 140.6356359024541689, 85.03908161011133870, 20.00000000000000000 ) ) ;
#13701=EDGE_CURVE ( 'NONE', #6080, #10198, #6042, .T. ) ;
#13712=LINE ( 'NONE', #11425, #2512 ) ;
#13723=EDGE_CURVE ( 'NONE', #11467, #1998, #12247, .T. ) ;
#13725=CYLINDRICAL_SURFACE ( 'NONE', #2762, 0.2500000000000002220 ) ;
#13738=CARTESIAN_POINT ( 'NONE',  ( 134.6356359024541973, 108.6554980190242503, 23.00000000000000000 ) ) ;
#13740=EDGE_CURVE ( 'NONE', #7715, #3533, #6269, .T. ) ;
#13747=VERTEX_POINT ( 'NONE', #5152 ) ;
#13748=ORIENTED_EDGE ( 'NONE', *, *, #3990, .T. ) ;
#13749=VERTEX_POINT ( 'NONE', #12488 ) ;
#13750=PLANE ( 'NONE',  #9296 ) ;
#13753=DIRECTION ( 'NONE',  ( 0.000000000000000000, 0.000000000000000000, 1.000000000000000000 ) ) ;
#13754=DIRECTION ( 'NONE',  ( -1.000000000000000000, 0.000000000000000000, 0.000000000000000000 ) ) ;
#13763=AXIS2_PLACEMENT_3D ( 'NONE', #2089, #4172, #7421 ) ;
#13772=DIRECTION ( 'NONE',  ( -1.000000000000000000, 0.000000000000000000, 0.000000000000000000 ) ) ;
#13773=DIRECTION ( 'NONE',  ( 0.000000000000000000, 0.000000000000000000, -1.000000000000000000 ) ) ;
#13775=DIRECTION ( 'NONE',  ( -0.000000000000000000, 1.000000000000000000, -0.000000000000000000 ) ) ;
#13781=AXIS2_PLACEMENT_3D ( 'NONE', #13304, #11986, #11922 ) ;
#13784=CARTESIAN_POINT ( 'NONE',  ( 76.11748380738829667, 115.4601262030644762, 0.7500000000000006661 ) ) ;
#13787=( NAMED_UNIT ( * ) PLANE_ANGLE_UNIT ( ) SI_UNIT ( $, .RADIAN. ) );
#13805=CARTESIAN_POINT ( 'NONE',  ( 42.63563590245419732, 87.03908161011136713, 19.25000000000000000 ) ) ;
ENDSEC;
END-ISO-10303-21;
